ISO-10303-21;
HEADER;
/* Generated by software containing ST-Developer
 * from STEP Tools, Inc. (www.steptools.com) 
 */

FILE_DESCRIPTION(
/* description */ ('STEP AP214'),
/* implementation_level */ '2;1');

FILE_NAME(
/* name */ 'Nut.step',
/* time_stamp */ '2026-11-14T21:32:33-08:00',
/* author */ (''),
/* organization */ (''),
/* preprocessor_version */ 'ST-DEVELOPER v20.2',
/* originating_system */ 'Autodesk Translation Framework v15.17.0.0',
/* authorisation */ '');

FILE_SCHEMA (('AUTOMOTIVE_DESIGN { 1 0 10303 214 3 1 1 }'));
ENDSEC;

DATA;
#10=MECHANICAL_DESIGN_GEOMETRIC_PRESENTATION_REPRESENTATION('',(#183),#10551);
#50=SPHERICAL_SURFACE('',#3737,2.525);
#51=SPHERICAL_SURFACE('',#3742,6.);
#52=SPHERICAL_SURFACE('',#3746,6.);
#53=SPHERICAL_SURFACE('',#3750,6.);
#54=SPHERICAL_SURFACE('',#3754,6.);
#55=SPHERICAL_SURFACE('',#3800,6.);
#56=SPHERICAL_SURFACE('',#3803,6.);
#57=SPHERICAL_SURFACE('',#3807,6.);
#58=SPHERICAL_SURFACE('',#3811,6.);
#59=SPHERICAL_SURFACE('',#3814,6.);
#60=SPHERICAL_SURFACE('',#3817,6.);
#61=SPHERICAL_SURFACE('',#3821,6.);
#62=SPHERICAL_SURFACE('',#3825,6.);
#63=SPHERICAL_SURFACE('',#3829,0.05);
#64=SPHERICAL_SURFACE('',#3845,0.05);
#65=SPHERICAL_SURFACE('',#3847,0.05);
#66=SPHERICAL_SURFACE('',#3849,0.05);
#67=SPHERICAL_SURFACE('',#3851,0.05);
#68=SPHERICAL_SURFACE('',#3873,0.05);
#69=SPHERICAL_SURFACE('',#3875,0.05);
#70=SPHERICAL_SURFACE('',#3877,0.05);
#71=SPHERICAL_SURFACE('',#3879,0.05);
#72=SPHERICAL_SURFACE('',#3881,0.05);
#73=SPHERICAL_SURFACE('',#3883,0.05);
#74=SPHERICAL_SURFACE('',#3903,0.05);
#75=SPHERICAL_SURFACE('',#3905,0.05);
#76=SPHERICAL_SURFACE('',#3907,0.05);
#77=SPHERICAL_SURFACE('',#3909,0.05);
#78=SPHERICAL_SURFACE('',#3911,0.05);
#79=SPHERICAL_SURFACE('',#3913,0.05);
#80=SPHERICAL_SURFACE('',#3936,0.05);
#81=SPHERICAL_SURFACE('',#3938,0.05);
#82=SPHERICAL_SURFACE('',#3941,0.05);
#83=SPHERICAL_SURFACE('',#3943,0.05);
#84=SPHERICAL_SURFACE('',#3945,0.05);
#85=SPHERICAL_SURFACE('',#3946,0.05);
#86=SPHERICAL_SURFACE('',#3948,0.05);
#87=SPHERICAL_SURFACE('',#3968,0.05);
#88=SPHERICAL_SURFACE('',#3970,0.05);
#89=SPHERICAL_SURFACE('',#3972,0.05);
#90=SPHERICAL_SURFACE('',#3974,0.05);
#91=SPHERICAL_SURFACE('',#3990,0.05);
#92=SPHERICAL_SURFACE('',#3992,0.05);
#93=SPHERICAL_SURFACE('',#3994,0.05);
#94=SPHERICAL_SURFACE('',#3996,0.05);
#95=SPHERICAL_SURFACE('',#4006,0.05);
#96=SPHERICAL_SURFACE('',#4008,0.05);
#97=TOROIDAL_SURFACE('',#3724,2.70416345659799,0.05);
#98=TOROIDAL_SURFACE('',#3732,2.70416345659799,0.05);
#99=TOROIDAL_SURFACE('',#3835,2.70416345659799,0.05);
#100=TOROIDAL_SURFACE('',#3837,5.32728824074688,0.05);
#101=TOROIDAL_SURFACE('',#3840,5.32728824074688,0.05);
#102=TOROIDAL_SURFACE('',#3842,5.32728824074688,0.05);
#103=TOROIDAL_SURFACE('',#3854,5.32728824074688,0.05);
#104=TOROIDAL_SURFACE('',#3856,2.70416345659799,0.05);
#105=TOROIDAL_SURFACE('',#3862,5.32728824074688,0.05);
#106=TOROIDAL_SURFACE('',#3868,5.32728824074688,0.05);
#107=TOROIDAL_SURFACE('',#3887,5.32728824074688,0.05);
#108=TOROIDAL_SURFACE('',#3890,5.32728824074688,0.05);
#109=TOROIDAL_SURFACE('',#3892,5.32728824074688,0.05);
#110=TOROIDAL_SURFACE('',#3894,2.70416345659799,0.05);
#111=TOROIDAL_SURFACE('',#3896,2.70416345659799,0.05);
#112=TOROIDAL_SURFACE('',#3898,5.32728824074688,0.05);
#113=TOROIDAL_SURFACE('',#3900,5.32728824074688,0.05);
#114=TOROIDAL_SURFACE('',#3915,5.32728824074688,0.05);
#115=TOROIDAL_SURFACE('',#3917,2.70416345659799,0.05);
#116=TOROIDAL_SURFACE('',#3919,2.70416345659799,0.05);
#117=TOROIDAL_SURFACE('',#3926,5.32728824074688,0.05);
#118=TOROIDAL_SURFACE('',#3933,5.32728824074688,0.05);
#119=TOROIDAL_SURFACE('',#3954,5.32728824074688,0.05);
#120=TOROIDAL_SURFACE('',#3956,5.32728824074688,0.05);
#121=TOROIDAL_SURFACE('',#3958,5.32728824074688,0.05);
#122=TOROIDAL_SURFACE('',#3960,2.70416345659799,0.05);
#123=TOROIDAL_SURFACE('',#3962,5.32728824074688,0.05);
#124=TOROIDAL_SURFACE('',#3964,5.32728824074688,0.05);
#125=TOROIDAL_SURFACE('',#3966,5.32728824074688,0.05);
#126=TOROIDAL_SURFACE('',#3978,5.32728824074688,0.05);
#127=TOROIDAL_SURFACE('',#3985,5.32728824074688,0.05);
#128=TOROIDAL_SURFACE('',#3998,5.32728824074688,0.05);
#129=TOROIDAL_SURFACE('',#4000,2.70416345659799,0.05);
#130=TOROIDAL_SURFACE('',#4002,2.70416345659799,0.05);
#131=TOROIDAL_SURFACE('',#4004,5.32728824074688,0.05);
#137=CONICAL_SURFACE('',#3719,1.15,0.785398163397453);
#148=B_SPLINE_CURVE_WITH_KNOTS('',3,(#8129,#8130,#8131,#8132,#8133,#8134,
#8135,#8136,#8137,#8138,#8139,#8140),.UNSPECIFIED.,.F.,.F.,(4,2,2,2,2,4),
(0.0241248766269512,0.0242510021276225,0.0244868094400705,0.0259331295349885,
0.0273794496299066,0.0302720898197427),.UNSPECIFIED.);
#149=B_SPLINE_CURVE_WITH_KNOTS('',3,(#8142,#8143,#8144,#8145,#8146,#8147,
#8148,#8149,#8150,#8151,#8152,#8153),.UNSPECIFIED.,.F.,.F.,(4,2,2,2,2,4),
(0.103445236849632,0.106337877040163,0.107784197135428,0.109230517230693,
0.109466324543198,0.109592450043899),.UNSPECIFIED.);
#165=SHAPE_REPRESENTATION_RELATIONSHIP('SRR','None',#10592,#174);
#174=ADVANCED_BREP_SHAPE_REPRESENTATION('',(#193),#10548);
#183=STYLED_ITEM('',(#10644),#193);
#193=MANIFOLD_SOLID_BREP('Body1',#3432);
#221=FACE_BOUND('',#658,.T.);
#222=FACE_BOUND('',#660,.T.);
#284=PLANE('',#3758);
#285=PLANE('',#3763);
#286=PLANE('',#3768);
#287=PLANE('',#3773);
#288=PLANE('',#3778);
#289=PLANE('',#3783);
#290=PLANE('',#3788);
#291=PLANE('',#3794);
#292=PLANE('',#4011);
#396=FACE_OUTER_BOUND('',#640,.T.);
#397=FACE_OUTER_BOUND('',#641,.T.);
#398=FACE_OUTER_BOUND('',#642,.T.);
#399=FACE_OUTER_BOUND('',#643,.T.);
#400=FACE_OUTER_BOUND('',#644,.T.);
#401=FACE_OUTER_BOUND('',#645,.T.);
#402=FACE_OUTER_BOUND('',#646,.T.);
#403=FACE_OUTER_BOUND('',#647,.T.);
#404=FACE_OUTER_BOUND('',#648,.T.);
#405=FACE_OUTER_BOUND('',#649,.T.);
#406=FACE_OUTER_BOUND('',#650,.T.);
#407=FACE_OUTER_BOUND('',#651,.T.);
#408=FACE_OUTER_BOUND('',#652,.T.);
#409=FACE_OUTER_BOUND('',#653,.T.);
#410=FACE_OUTER_BOUND('',#654,.T.);
#411=FACE_OUTER_BOUND('',#655,.T.);
#412=FACE_OUTER_BOUND('',#656,.T.);
#413=FACE_OUTER_BOUND('',#657,.T.);
#414=FACE_OUTER_BOUND('',#659,.T.);
#415=FACE_OUTER_BOUND('',#661,.T.);
#416=FACE_OUTER_BOUND('',#662,.T.);
#417=FACE_OUTER_BOUND('',#663,.T.);
#418=FACE_OUTER_BOUND('',#664,.T.);
#419=FACE_OUTER_BOUND('',#665,.T.);
#420=FACE_OUTER_BOUND('',#666,.T.);
#421=FACE_OUTER_BOUND('',#667,.T.);
#422=FACE_OUTER_BOUND('',#668,.T.);
#423=FACE_OUTER_BOUND('',#669,.T.);
#424=FACE_OUTER_BOUND('',#670,.T.);
#425=FACE_OUTER_BOUND('',#671,.T.);
#426=FACE_OUTER_BOUND('',#672,.T.);
#427=FACE_OUTER_BOUND('',#673,.T.);
#428=FACE_OUTER_BOUND('',#674,.T.);
#429=FACE_OUTER_BOUND('',#675,.T.);
#430=FACE_OUTER_BOUND('',#676,.T.);
#431=FACE_OUTER_BOUND('',#677,.T.);
#432=FACE_OUTER_BOUND('',#678,.T.);
#433=FACE_OUTER_BOUND('',#679,.T.);
#434=FACE_OUTER_BOUND('',#680,.T.);
#435=FACE_OUTER_BOUND('',#681,.T.);
#436=FACE_OUTER_BOUND('',#682,.T.);
#437=FACE_OUTER_BOUND('',#683,.T.);
#438=FACE_OUTER_BOUND('',#684,.T.);
#439=FACE_OUTER_BOUND('',#685,.T.);
#440=FACE_OUTER_BOUND('',#686,.T.);
#441=FACE_OUTER_BOUND('',#687,.T.);
#442=FACE_OUTER_BOUND('',#688,.T.);
#443=FACE_OUTER_BOUND('',#689,.T.);
#444=FACE_OUTER_BOUND('',#690,.T.);
#445=FACE_OUTER_BOUND('',#691,.T.);
#446=FACE_OUTER_BOUND('',#692,.T.);
#447=FACE_OUTER_BOUND('',#693,.T.);
#448=FACE_OUTER_BOUND('',#694,.T.);
#449=FACE_OUTER_BOUND('',#695,.T.);
#450=FACE_OUTER_BOUND('',#696,.T.);
#451=FACE_OUTER_BOUND('',#697,.T.);
#452=FACE_OUTER_BOUND('',#698,.T.);
#453=FACE_OUTER_BOUND('',#699,.T.);
#454=FACE_OUTER_BOUND('',#700,.T.);
#455=FACE_OUTER_BOUND('',#701,.T.);
#456=FACE_OUTER_BOUND('',#702,.T.);
#457=FACE_OUTER_BOUND('',#703,.T.);
#458=FACE_OUTER_BOUND('',#704,.T.);
#459=FACE_OUTER_BOUND('',#705,.T.);
#460=FACE_OUTER_BOUND('',#706,.T.);
#461=FACE_OUTER_BOUND('',#707,.T.);
#462=FACE_OUTER_BOUND('',#708,.T.);
#463=FACE_OUTER_BOUND('',#709,.T.);
#464=FACE_OUTER_BOUND('',#710,.T.);
#465=FACE_OUTER_BOUND('',#711,.T.);
#466=FACE_OUTER_BOUND('',#712,.T.);
#467=FACE_OUTER_BOUND('',#713,.T.);
#468=FACE_OUTER_BOUND('',#714,.T.);
#469=FACE_OUTER_BOUND('',#715,.T.);
#470=FACE_OUTER_BOUND('',#716,.T.);
#471=FACE_OUTER_BOUND('',#717,.T.);
#472=FACE_OUTER_BOUND('',#718,.T.);
#473=FACE_OUTER_BOUND('',#719,.T.);
#474=FACE_OUTER_BOUND('',#720,.T.);
#475=FACE_OUTER_BOUND('',#721,.T.);
#476=FACE_OUTER_BOUND('',#722,.T.);
#477=FACE_OUTER_BOUND('',#723,.T.);
#478=FACE_OUTER_BOUND('',#724,.T.);
#479=FACE_OUTER_BOUND('',#725,.T.);
#480=FACE_OUTER_BOUND('',#726,.T.);
#481=FACE_OUTER_BOUND('',#727,.T.);
#482=FACE_OUTER_BOUND('',#728,.T.);
#483=FACE_OUTER_BOUND('',#729,.T.);
#484=FACE_OUTER_BOUND('',#730,.T.);
#485=FACE_OUTER_BOUND('',#731,.T.);
#486=FACE_OUTER_BOUND('',#732,.T.);
#487=FACE_OUTER_BOUND('',#733,.T.);
#488=FACE_OUTER_BOUND('',#734,.T.);
#489=FACE_OUTER_BOUND('',#735,.T.);
#490=FACE_OUTER_BOUND('',#736,.T.);
#491=FACE_OUTER_BOUND('',#737,.T.);
#492=FACE_OUTER_BOUND('',#738,.T.);
#493=FACE_OUTER_BOUND('',#739,.T.);
#494=FACE_OUTER_BOUND('',#740,.T.);
#495=FACE_OUTER_BOUND('',#741,.T.);
#496=FACE_OUTER_BOUND('',#742,.T.);
#497=FACE_OUTER_BOUND('',#743,.T.);
#498=FACE_OUTER_BOUND('',#744,.T.);
#499=FACE_OUTER_BOUND('',#745,.T.);
#500=FACE_OUTER_BOUND('',#746,.T.);
#501=FACE_OUTER_BOUND('',#747,.T.);
#502=FACE_OUTER_BOUND('',#748,.T.);
#503=FACE_OUTER_BOUND('',#749,.T.);
#504=FACE_OUTER_BOUND('',#750,.T.);
#505=FACE_OUTER_BOUND('',#751,.T.);
#506=FACE_OUTER_BOUND('',#752,.T.);
#507=FACE_OUTER_BOUND('',#753,.T.);
#640=EDGE_LOOP('',(#2678,#2679,#2680,#2681));
#641=EDGE_LOOP('',(#2682,#2683,#2684,#2685));
#642=EDGE_LOOP('',(#2686,#2687,#2688,#2689));
#643=EDGE_LOOP('',(#2690,#2691,#2692,#2693));
#644=EDGE_LOOP('',(#2694,#2695,#2696,#2697));
#645=EDGE_LOOP('',(#2698,#2699,#2700));
#646=EDGE_LOOP('',(#2701,#2702,#2703,#2704));
#647=EDGE_LOOP('',(#2705,#2706,#2707));
#648=EDGE_LOOP('',(#2708,#2709,#2710));
#649=EDGE_LOOP('',(#2711,#2712,#2713));
#650=EDGE_LOOP('',(#2714,#2715,#2716));
#651=EDGE_LOOP('',(#2717,#2718,#2719,#2720,#2721,#2722,#2723,#2724));
#652=EDGE_LOOP('',(#2725,#2726,#2727,#2728,#2729,#2730,#2731,#2732));
#653=EDGE_LOOP('',(#2733,#2734,#2735,#2736,#2737,#2738,#2739,#2740));
#654=EDGE_LOOP('',(#2741,#2742,#2743,#2744,#2745,#2746,#2747,#2748));
#655=EDGE_LOOP('',(#2749,#2750,#2751,#2752,#2753,#2754,#2755,#2756));
#656=EDGE_LOOP('',(#2757,#2758,#2759,#2760,#2761,#2762,#2763,#2764));
#657=EDGE_LOOP('',(#2765,#2766,#2767,#2768,#2769,#2770,#2771,#2772,#2773,
#2774,#2775,#2776));
#658=EDGE_LOOP('',(#2777));
#659=EDGE_LOOP('',(#2778,#2779,#2780,#2781,#2782,#2783,#2784,#2785,#2786,
#2787,#2788,#2789));
#660=EDGE_LOOP('',(#2790));
#661=EDGE_LOOP('',(#2791,#2792,#2793));
#662=EDGE_LOOP('',(#2794,#2795,#2796));
#663=EDGE_LOOP('',(#2797,#2798,#2799));
#664=EDGE_LOOP('',(#2800,#2801,#2802,#2803,#2804));
#665=EDGE_LOOP('',(#2805,#2806,#2807));
#666=EDGE_LOOP('',(#2808,#2809,#2810));
#667=EDGE_LOOP('',(#2811,#2812,#2813));
#668=EDGE_LOOP('',(#2814,#2815,#2816));
#669=EDGE_LOOP('',(#2817,#2818,#2819));
#670=EDGE_LOOP('',(#2820,#2821,#2822,#2823));
#671=EDGE_LOOP('',(#2824,#2825,#2826,#2827));
#672=EDGE_LOOP('',(#2828,#2829,#2830,#2831));
#673=EDGE_LOOP('',(#2832,#2833,#2834,#2835));
#674=EDGE_LOOP('',(#2836,#2837,#2838,#2839));
#675=EDGE_LOOP('',(#2840,#2841,#2842));
#676=EDGE_LOOP('',(#2843,#2844,#2845));
#677=EDGE_LOOP('',(#2846,#2847,#2848));
#678=EDGE_LOOP('',(#2849,#2850,#2851));
#679=EDGE_LOOP('',(#2852,#2853,#2854,#2855));
#680=EDGE_LOOP('',(#2856,#2857,#2858,#2859));
#681=EDGE_LOOP('',(#2860,#2861,#2862,#2863));
#682=EDGE_LOOP('',(#2864,#2865,#2866,#2867));
#683=EDGE_LOOP('',(#2868,#2869,#2870,#2871));
#684=EDGE_LOOP('',(#2872,#2873,#2874,#2875));
#685=EDGE_LOOP('',(#2876,#2877,#2878,#2879));
#686=EDGE_LOOP('',(#2880,#2881,#2882,#2883));
#687=EDGE_LOOP('',(#2884,#2885,#2886));
#688=EDGE_LOOP('',(#2887,#2888,#2889));
#689=EDGE_LOOP('',(#2890,#2891,#2892));
#690=EDGE_LOOP('',(#2893,#2894,#2895));
#691=EDGE_LOOP('',(#2896,#2897,#2898));
#692=EDGE_LOOP('',(#2899,#2900,#2901));
#693=EDGE_LOOP('',(#2902,#2903,#2904,#2905));
#694=EDGE_LOOP('',(#2906,#2907,#2908,#2909));
#695=EDGE_LOOP('',(#2910,#2911,#2912,#2913));
#696=EDGE_LOOP('',(#2914,#2915,#2916,#2917));
#697=EDGE_LOOP('',(#2918,#2919,#2920,#2921));
#698=EDGE_LOOP('',(#2922,#2923,#2924,#2925));
#699=EDGE_LOOP('',(#2926,#2927,#2928,#2929));
#700=EDGE_LOOP('',(#2930,#2931,#2932,#2933));
#701=EDGE_LOOP('',(#2934,#2935,#2936));
#702=EDGE_LOOP('',(#2937,#2938,#2939));
#703=EDGE_LOOP('',(#2940,#2941,#2942));
#704=EDGE_LOOP('',(#2943,#2944,#2945));
#705=EDGE_LOOP('',(#2946,#2947,#2948));
#706=EDGE_LOOP('',(#2949,#2950,#2951));
#707=EDGE_LOOP('',(#2952,#2953,#2954,#2955));
#708=EDGE_LOOP('',(#2956,#2957,#2958,#2959));
#709=EDGE_LOOP('',(#2960,#2961,#2962,#2963));
#710=EDGE_LOOP('',(#2964,#2965,#2966,#2967));
#711=EDGE_LOOP('',(#2968,#2969,#2970,#2971));
#712=EDGE_LOOP('',(#2972,#2973,#2974,#2975));
#713=EDGE_LOOP('',(#2976,#2977,#2978,#2979));
#714=EDGE_LOOP('',(#2980,#2981,#2982,#2983));
#715=EDGE_LOOP('',(#2984,#2985,#2986,#2987));
#716=EDGE_LOOP('',(#2988,#2989,#2990));
#717=EDGE_LOOP('',(#2991,#2992,#2993));
#718=EDGE_LOOP('',(#2994,#2995,#2996));
#719=EDGE_LOOP('',(#2997,#2998,#2999));
#720=EDGE_LOOP('',(#3000,#3001,#3002));
#721=EDGE_LOOP('',(#3003,#3004,#3005));
#722=EDGE_LOOP('',(#3006,#3007,#3008));
#723=EDGE_LOOP('',(#3009,#3010,#3011,#3012,#3013));
#724=EDGE_LOOP('',(#3014,#3015,#3016,#3017,#3018));
#725=EDGE_LOOP('',(#3019,#3020,#3021,#3022));
#726=EDGE_LOOP('',(#3023,#3024,#3025,#3026));
#727=EDGE_LOOP('',(#3027,#3028,#3029,#3030));
#728=EDGE_LOOP('',(#3031,#3032,#3033,#3034));
#729=EDGE_LOOP('',(#3035,#3036,#3037,#3038));
#730=EDGE_LOOP('',(#3039,#3040,#3041,#3042));
#731=EDGE_LOOP('',(#3043,#3044,#3045,#3046));
#732=EDGE_LOOP('',(#3047,#3048,#3049));
#733=EDGE_LOOP('',(#3050,#3051,#3052));
#734=EDGE_LOOP('',(#3053,#3054,#3055));
#735=EDGE_LOOP('',(#3056,#3057,#3058));
#736=EDGE_LOOP('',(#3059,#3060,#3061,#3062));
#737=EDGE_LOOP('',(#3063,#3064,#3065,#3066));
#738=EDGE_LOOP('',(#3067,#3068,#3069,#3070));
#739=EDGE_LOOP('',(#3071,#3072,#3073,#3074));
#740=EDGE_LOOP('',(#3075,#3076,#3077,#3078));
#741=EDGE_LOOP('',(#3079,#3080,#3081,#3082));
#742=EDGE_LOOP('',(#3083,#3084,#3085));
#743=EDGE_LOOP('',(#3086,#3087,#3088));
#744=EDGE_LOOP('',(#3089,#3090,#3091));
#745=EDGE_LOOP('',(#3092,#3093,#3094));
#746=EDGE_LOOP('',(#3095,#3096,#3097,#3098));
#747=EDGE_LOOP('',(#3099,#3100,#3101,#3102));
#748=EDGE_LOOP('',(#3103,#3104,#3105,#3106));
#749=EDGE_LOOP('',(#3107,#3108,#3109,#3110));
#750=EDGE_LOOP('',(#3111,#3112,#3113));
#751=EDGE_LOOP('',(#3114,#3115,#3116));
#752=EDGE_LOOP('',(#3117,#3118,#3119,#3120));
#753=EDGE_LOOP('',(#3121));
#919=LINE('',#7897,#1116);
#920=LINE('',#7902,#1117);
#921=LINE('',#7917,#1118);
#922=LINE('',#7920,#1119);
#923=LINE('',#7938,#1120);
#924=LINE('',#7970,#1121);
#925=LINE('',#7974,#1122);
#926=LINE('',#7978,#1123);
#927=LINE('',#7982,#1124);
#928=LINE('',#7989,#1125);
#929=LINE('',#7993,#1126);
#930=LINE('',#7997,#1127);
#931=LINE('',#8000,#1128);
#932=LINE('',#8006,#1129);
#933=LINE('',#8010,#1130);
#934=LINE('',#8014,#1131);
#935=LINE('',#8017,#1132);
#936=LINE('',#8023,#1133);
#937=LINE('',#8027,#1134);
#938=LINE('',#8031,#1135);
#939=LINE('',#8034,#1136);
#940=LINE('',#8039,#1137);
#941=LINE('',#8043,#1138);
#942=LINE('',#8047,#1139);
#943=LINE('',#8054,#1140);
#944=LINE('',#8059,#1141);
#945=LINE('',#8062,#1142);
#946=LINE('',#8068,#1143);
#947=LINE('',#8071,#1144);
#948=LINE('',#8073,#1145);
#949=LINE('',#8077,#1146);
#950=LINE('',#8081,#1147);
#951=LINE('',#8084,#1148);
#952=LINE('',#8088,#1149);
#953=LINE('',#8091,#1150);
#954=LINE('',#8093,#1151);
#955=LINE('',#8097,#1152);
#956=LINE('',#8101,#1153);
#957=LINE('',#8105,#1154);
#1116=VECTOR('',#4564,1.15);
#1117=VECTOR('',#4571,1.15);
#1118=VECTOR('',#4586,1000.);
#1119=VECTOR('',#4589,1000.);
#1120=VECTOR('',#4610,2.525);
#1121=VECTOR('',#4645,1000.);
#1122=VECTOR('',#4648,1000.);
#1123=VECTOR('',#4651,1000.);
#1124=VECTOR('',#4654,1000.);
#1125=VECTOR('',#4661,1000.);
#1126=VECTOR('',#4664,1000.);
#1127=VECTOR('',#4667,1000.);
#1128=VECTOR('',#4670,1000.);
#1129=VECTOR('',#4675,1000.);
#1130=VECTOR('',#4678,1000.);
#1131=VECTOR('',#4681,1000.);
#1132=VECTOR('',#4684,1000.);
#1133=VECTOR('',#4689,1000.);
#1134=VECTOR('',#4692,1000.);
#1135=VECTOR('',#4695,1000.);
#1136=VECTOR('',#4698,1000.);
#1137=VECTOR('',#4703,1000.);
#1138=VECTOR('',#4706,1000.);
#1139=VECTOR('',#4709,1000.);
#1140=VECTOR('',#4716,1000.);
#1141=VECTOR('',#4721,1000.);
#1142=VECTOR('',#4724,1000.);
#1143=VECTOR('',#4729,1000.);
#1144=VECTOR('',#4732,1000.);
#1145=VECTOR('',#4733,1000.);
#1146=VECTOR('',#4736,1000.);
#1147=VECTOR('',#4739,1000.);
#1148=VECTOR('',#4742,1000.);
#1149=VECTOR('',#4745,1000.);
#1150=VECTOR('',#4748,1000.);
#1151=VECTOR('',#4749,1000.);
#1152=VECTOR('',#4752,1000.);
#1153=VECTOR('',#4755,1000.);
#1154=VECTOR('',#4758,1000.);
#1232=CIRCLE('',#3720,1.15);
#1233=CIRCLE('',#3721,1.35);
#1234=CIRCLE('',#3723,1.15);
#1235=CIRCLE('',#3725,2.70416345659799);
#1236=CIRCLE('',#3726,0.05);
#1237=CIRCLE('',#3727,2.72688751925848);
#1238=CIRCLE('',#3728,0.0499999999999998);
#1239=CIRCLE('',#3730,0.05);
#1240=CIRCLE('',#3731,0.05);
#1241=CIRCLE('',#3733,2.72688751925848);
#1242=CIRCLE('',#3734,0.0500000000000001);
#1243=CIRCLE('',#3735,2.70416345659799);
#1244=CIRCLE('',#3736,0.0499999999999998);
#1245=CIRCLE('',#3738,2.525);
#1246=CIRCLE('',#3739,2.525);
#1247=CIRCLE('',#3741,2.525);
#1248=CIRCLE('',#3743,2.72688751925848);
#1249=CIRCLE('',#3744,5.37205536882039);
#1250=CIRCLE('',#3745,5.37205536882038);
#1251=CIRCLE('',#3747,2.72688751925848);
#1252=CIRCLE('',#3748,5.37205536882038);
#1253=CIRCLE('',#3749,5.37205536882038);
#1254=CIRCLE('',#3751,2.72688751925848);
#1255=CIRCLE('',#3752,5.37205536882039);
#1256=CIRCLE('',#3753,5.37205536882039);
#1257=CIRCLE('',#3755,2.72688751925848);
#1258=CIRCLE('',#3756,5.37205536882039);
#1259=CIRCLE('',#3757,5.37205536882038);
#1260=CIRCLE('',#3759,5.32728824074688);
#1261=CIRCLE('',#3760,5.32728824074688);
#1262=CIRCLE('',#3761,5.32728824074688);
#1263=CIRCLE('',#3762,5.32728824074688);
#1264=CIRCLE('',#3764,5.32728824074688);
#1265=CIRCLE('',#3765,5.32728824074688);
#1266=CIRCLE('',#3766,5.32728824074688);
#1267=CIRCLE('',#3767,5.32728824074688);
#1268=CIRCLE('',#3769,5.32728824074688);
#1269=CIRCLE('',#3770,5.32728824074688);
#1270=CIRCLE('',#3771,5.32728824074688);
#1271=CIRCLE('',#3772,5.32728824074688);
#1272=CIRCLE('',#3774,5.32728824074688);
#1273=CIRCLE('',#3775,5.32728824074688);
#1274=CIRCLE('',#3776,5.32728824074688);
#1275=CIRCLE('',#3777,5.32728824074688);
#1276=CIRCLE('',#3779,5.32728824074688);
#1277=CIRCLE('',#3780,5.32728824074688);
#1278=CIRCLE('',#3781,5.32728824074688);
#1279=CIRCLE('',#3782,5.32728824074688);
#1280=CIRCLE('',#3784,5.32728824074688);
#1281=CIRCLE('',#3785,5.32728824074688);
#1282=CIRCLE('',#3786,5.32728824074688);
#1283=CIRCLE('',#3787,5.32728824074688);
#1284=CIRCLE('',#3789,2.71615537110821);
#1285=CIRCLE('',#3790,2.70416345659799);
#1286=CIRCLE('',#3791,2.70416345659799);
#1287=CIRCLE('',#3792,2.70416345659799);
#1288=CIRCLE('',#3793,2.70416345659799);
#1289=CIRCLE('',#3795,2.70416345659799);
#1290=CIRCLE('',#3796,2.70416345659799);
#1291=CIRCLE('',#3797,2.70416345659799);
#1292=CIRCLE('',#3798,2.70416345659799);
#1293=CIRCLE('',#3799,2.70416345659799);
#1294=CIRCLE('',#3801,5.37205536882039);
#1295=CIRCLE('',#3802,5.37205536882038);
#1296=CIRCLE('',#3804,5.37205536882039);
#1297=CIRCLE('',#3805,5.37205536882038);
#1298=CIRCLE('',#3806,2.72688751925848);
#1299=CIRCLE('',#3808,5.37205536882038);
#1300=CIRCLE('',#3809,5.37205536882038);
#1301=CIRCLE('',#3810,2.72688751925848);
#1302=CIRCLE('',#3812,5.37205536882038);
#1303=CIRCLE('',#3813,5.37205536882039);
#1304=CIRCLE('',#3815,5.37205536882039);
#1305=CIRCLE('',#3816,5.37205536882038);
#1306=CIRCLE('',#3818,2.72688751925848);
#1307=CIRCLE('',#3819,5.37205536882038);
#1308=CIRCLE('',#3820,5.37205536882039);
#1309=CIRCLE('',#3822,2.72688751925848);
#1310=CIRCLE('',#3823,5.37205536882039);
#1311=CIRCLE('',#3824,5.37205536882038);
#1312=CIRCLE('',#3826,2.72688751925848);
#1313=CIRCLE('',#3827,5.37205536882039);
#1314=CIRCLE('',#3828,5.37205536882039);
#1315=CIRCLE('',#3830,0.0499999999999999);
#1316=CIRCLE('',#3831,0.0500000000000001);
#1317=CIRCLE('',#3832,0.05);
#1318=CIRCLE('',#3834,0.0500000000000001);
#1319=CIRCLE('',#3836,0.0500000000000001);
#1320=CIRCLE('',#3838,0.0499999999999998);
#1321=CIRCLE('',#3839,0.0500000000000002);
#1322=CIRCLE('',#3841,0.0499999999999999);
#1323=CIRCLE('',#3843,0.0500000000000002);
#1324=CIRCLE('',#3844,0.05);
#1325=CIRCLE('',#3846,0.0500000000000001);
#1326=CIRCLE('',#3848,0.0499999999999999);
#1327=CIRCLE('',#3850,0.0499999999999999);
#1328=CIRCLE('',#3852,0.0499999999999999);
#1329=CIRCLE('',#3853,0.05);
#1330=CIRCLE('',#3855,0.05);
#1331=CIRCLE('',#3857,0.0499999999999998);
#1332=CIRCLE('',#3859,0.0500000000000001);
#1333=CIRCLE('',#3861,0.0499999999999999);
#1334=CIRCLE('',#3863,0.05);
#1335=CIRCLE('',#3864,0.0500000000000001);
#1336=CIRCLE('',#3866,0.05);
#1337=CIRCLE('',#3867,0.0500000000000001);
#1338=CIRCLE('',#3869,0.05);
#1339=CIRCLE('',#3870,0.05);
#1340=CIRCLE('',#3872,0.0500000000000001);
#1341=CIRCLE('',#3874,0.0500000000000002);
#1342=CIRCLE('',#3876,0.0500000000000001);
#1343=CIRCLE('',#3878,0.05);
#1344=CIRCLE('',#3880,0.0499999999999999);
#1345=CIRCLE('',#3882,0.0499999999999999);
#1346=CIRCLE('',#3884,0.05);
#1347=CIRCLE('',#3886,0.05);
#1348=CIRCLE('',#3888,0.0500000000000001);
#1349=CIRCLE('',#3889,0.0500000000000001);
#1350=CIRCLE('',#3891,0.0500000000000001);
#1351=CIRCLE('',#3893,0.0500000000000002);
#1352=CIRCLE('',#3895,0.0499999999999999);
#1353=CIRCLE('',#3897,0.0500000000000001);
#1354=CIRCLE('',#3899,0.0500000000000001);
#1355=CIRCLE('',#3901,0.0500000000000001);
#1356=CIRCLE('',#3902,0.0499999999999999);
#1357=CIRCLE('',#3904,0.0500000000000001);
#1358=CIRCLE('',#3906,0.05);
#1359=CIRCLE('',#3908,0.05);
#1360=CIRCLE('',#3910,0.0500000000000002);
#1361=CIRCLE('',#3912,0.0500000000000002);
#1362=CIRCLE('',#3914,0.0499999999999999);
#1363=CIRCLE('',#3916,0.0500000000000001);
#1364=CIRCLE('',#3918,0.0500000000000001);
#1365=CIRCLE('',#3920,0.0499999999999999);
#1366=CIRCLE('',#3921,0.0500000000000001);
#1367=CIRCLE('',#3923,0.0500000000000002);
#1368=CIRCLE('',#3925,0.05);
#1369=CIRCLE('',#3927,0.0500000000000001);
#1370=CIRCLE('',#3928,0.0499999999999999);
#1371=CIRCLE('',#3930,0.0500000000000001);
#1372=CIRCLE('',#3932,0.0500000000000001);
#1373=CIRCLE('',#3934,0.0500000000000001);
#1374=CIRCLE('',#3935,0.0500000000000001);
#1375=CIRCLE('',#3937,0.0500000000000001);
#1376=CIRCLE('',#3939,0.0500000000000002);
#1377=CIRCLE('',#3940,0.0500000000000001);
#1378=CIRCLE('',#3942,0.05);
#1379=CIRCLE('',#3944,0.05);
#1380=CIRCLE('',#3947,0.05);
#1381=CIRCLE('',#3949,0.0500000000000001);
#1382=CIRCLE('',#3951,0.0500702725160199);
#1383=CIRCLE('',#3953,0.0500702740290074);
#1384=CIRCLE('',#3955,0.05);
#1385=CIRCLE('',#3957,0.05);
#1386=CIRCLE('',#3959,0.05);
#1387=CIRCLE('',#3961,0.0500000000000001);
#1388=CIRCLE('',#3963,0.0500000000000001);
#1389=CIRCLE('',#3965,0.0499999999999999);
#1390=CIRCLE('',#3967,0.0499999999999998);
#1391=CIRCLE('',#3969,0.0499999999999999);
#1392=CIRCLE('',#3971,0.0500000000000001);
#1393=CIRCLE('',#3973,0.0500000000000001);
#1394=CIRCLE('',#3975,0.0500000000000001);
#1395=CIRCLE('',#3977,0.0500000000000001);
#1396=CIRCLE('',#3979,0.0500000000000002);
#1397=CIRCLE('',#3980,0.05);
#1398=CIRCLE('',#3982,0.0500000000000001);
#1399=CIRCLE('',#3984,0.0500000000000002);
#1400=CIRCLE('',#3986,0.05);
#1401=CIRCLE('',#3987,0.0500000000000002);
#1402=CIRCLE('',#3989,0.0499999999999999);
#1403=CIRCLE('',#3991,0.05);
#1404=CIRCLE('',#3993,0.0500000000000002);
#1405=CIRCLE('',#3995,0.0499999999999999);
#1406=CIRCLE('',#3997,0.05);
#1407=CIRCLE('',#3999,0.05);
#1408=CIRCLE('',#4001,0.0499999999999999);
#1409=CIRCLE('',#4003,0.0499999999999999);
#1410=CIRCLE('',#4005,0.05);
#1411=CIRCLE('',#4007,0.05);
#1412=CIRCLE('',#4009,0.0500000000000001);
#1584=VERTEX_POINT('',#7894);
#1585=VERTEX_POINT('',#7896);
#1586=VERTEX_POINT('',#7900);
#1587=VERTEX_POINT('',#7904);
#1588=VERTEX_POINT('',#7905);
#1589=VERTEX_POINT('',#7907);
#1590=VERTEX_POINT('',#7909);
#1591=VERTEX_POINT('',#7913);
#1592=VERTEX_POINT('',#7914);
#1593=VERTEX_POINT('',#7916);
#1594=VERTEX_POINT('',#7918);
#1595=VERTEX_POINT('',#7922);
#1596=VERTEX_POINT('',#7923);
#1597=VERTEX_POINT('',#7925);
#1598=VERTEX_POINT('',#7927);
#1599=VERTEX_POINT('',#7931);
#1600=VERTEX_POINT('',#7933);
#1601=VERTEX_POINT('',#7936);
#1602=VERTEX_POINT('',#7940);
#1603=VERTEX_POINT('',#7941);
#1604=VERTEX_POINT('',#7943);
#1605=VERTEX_POINT('',#7947);
#1606=VERTEX_POINT('',#7948);
#1607=VERTEX_POINT('',#7950);
#1608=VERTEX_POINT('',#7954);
#1609=VERTEX_POINT('',#7955);
#1610=VERTEX_POINT('',#7957);
#1611=VERTEX_POINT('',#7961);
#1612=VERTEX_POINT('',#7962);
#1613=VERTEX_POINT('',#7964);
#1614=VERTEX_POINT('',#7968);
#1615=VERTEX_POINT('',#7969);
#1616=VERTEX_POINT('',#7971);
#1617=VERTEX_POINT('',#7973);
#1618=VERTEX_POINT('',#7975);
#1619=VERTEX_POINT('',#7977);
#1620=VERTEX_POINT('',#7979);
#1621=VERTEX_POINT('',#7981);
#1622=VERTEX_POINT('',#7985);
#1623=VERTEX_POINT('',#7986);
#1624=VERTEX_POINT('',#7988);
#1625=VERTEX_POINT('',#7990);
#1626=VERTEX_POINT('',#7992);
#1627=VERTEX_POINT('',#7994);
#1628=VERTEX_POINT('',#7996);
#1629=VERTEX_POINT('',#7998);
#1630=VERTEX_POINT('',#8002);
#1631=VERTEX_POINT('',#8003);
#1632=VERTEX_POINT('',#8005);
#1633=VERTEX_POINT('',#8007);
#1634=VERTEX_POINT('',#8009);
#1635=VERTEX_POINT('',#8011);
#1636=VERTEX_POINT('',#8013);
#1637=VERTEX_POINT('',#8015);
#1638=VERTEX_POINT('',#8019);
#1639=VERTEX_POINT('',#8020);
#1640=VERTEX_POINT('',#8022);
#1641=VERTEX_POINT('',#8024);
#1642=VERTEX_POINT('',#8026);
#1643=VERTEX_POINT('',#8028);
#1644=VERTEX_POINT('',#8030);
#1645=VERTEX_POINT('',#8032);
#1646=VERTEX_POINT('',#8036);
#1647=VERTEX_POINT('',#8038);
#1648=VERTEX_POINT('',#8040);
#1649=VERTEX_POINT('',#8042);
#1650=VERTEX_POINT('',#8044);
#1651=VERTEX_POINT('',#8046);
#1652=VERTEX_POINT('',#8050);
#1653=VERTEX_POINT('',#8051);
#1654=VERTEX_POINT('',#8053);
#1655=VERTEX_POINT('',#8056);
#1656=VERTEX_POINT('',#8058);
#1657=VERTEX_POINT('',#8060);
#1658=VERTEX_POINT('',#8064);
#1659=VERTEX_POINT('',#8065);
#1660=VERTEX_POINT('',#8067);
#1661=VERTEX_POINT('',#8069);
#1662=VERTEX_POINT('',#8072);
#1663=VERTEX_POINT('',#8074);
#1664=VERTEX_POINT('',#8076);
#1665=VERTEX_POINT('',#8078);
#1666=VERTEX_POINT('',#8080);
#1667=VERTEX_POINT('',#8082);
#1668=VERTEX_POINT('',#8086);
#1669=VERTEX_POINT('',#8087);
#1670=VERTEX_POINT('',#8089);
#1671=VERTEX_POINT('',#8092);
#1672=VERTEX_POINT('',#8094);
#1673=VERTEX_POINT('',#8096);
#1674=VERTEX_POINT('',#8098);
#1675=VERTEX_POINT('',#8100);
#1676=VERTEX_POINT('',#8102);
#1677=VERTEX_POINT('',#8104);
#1678=VERTEX_POINT('',#8108);
#1679=VERTEX_POINT('',#8112);
#1680=VERTEX_POINT('',#8113);
#1681=VERTEX_POINT('',#8115);
#1682=VERTEX_POINT('',#8119);
#1683=VERTEX_POINT('',#8120);
#1684=VERTEX_POINT('',#8122);
#1685=VERTEX_POINT('',#8126);
#1686=VERTEX_POINT('',#8127);
#1687=VERTEX_POINT('',#8141);
#1688=VERTEX_POINT('',#8156);
#1689=VERTEX_POINT('',#8160);
#1690=VERTEX_POINT('',#8161);
#1691=VERTEX_POINT('',#8163);
#1692=VERTEX_POINT('',#8167);
#1693=VERTEX_POINT('',#8168);
#1694=VERTEX_POINT('',#8170);
#1695=VERTEX_POINT('',#8174);
#1696=VERTEX_POINT('',#8175);
#1697=VERTEX_POINT('',#8177);
#1952=EDGE_CURVE('',#1584,#1584,#1232,.T.);
#1953=EDGE_CURVE('',#1584,#1585,#919,.T.);
#1954=EDGE_CURVE('',#1585,#1585,#1233,.T.);
#1955=EDGE_CURVE('',#1586,#1586,#1234,.T.);
#1956=EDGE_CURVE('',#1586,#1584,#920,.T.);
#1957=EDGE_CURVE('',#1587,#1588,#1235,.T.);
#1958=EDGE_CURVE('',#1587,#1589,#1236,.T.);
#1959=EDGE_CURVE('',#1590,#1589,#1237,.T.);
#1960=EDGE_CURVE('',#1588,#1590,#1238,.T.);
#1961=EDGE_CURVE('',#1591,#1592,#1239,.T.);
#1962=EDGE_CURVE('',#1593,#1592,#921,.T.);
#1963=EDGE_CURVE('',#1594,#1593,#1240,.T.);
#1964=EDGE_CURVE('',#1591,#1594,#922,.T.);
#1965=EDGE_CURVE('',#1595,#1596,#1241,.T.);
#1966=EDGE_CURVE('',#1595,#1597,#1242,.T.);
#1967=EDGE_CURVE('',#1598,#1597,#1243,.T.);
#1968=EDGE_CURVE('',#1596,#1598,#1244,.T.);
#1969=EDGE_CURVE('',#1599,#1599,#1245,.T.);
#1970=EDGE_CURVE('',#1600,#1599,#1246,.T.);
#1971=EDGE_CURVE('',#1601,#1601,#1247,.T.);
#1972=EDGE_CURVE('',#1601,#1599,#923,.T.);
#1973=EDGE_CURVE('',#1602,#1603,#1248,.T.);
#1974=EDGE_CURVE('',#1603,#1604,#1249,.T.);
#1975=EDGE_CURVE('',#1604,#1602,#1250,.T.);
#1976=EDGE_CURVE('',#1605,#1606,#1251,.T.);
#1977=EDGE_CURVE('',#1606,#1607,#1252,.T.);
#1978=EDGE_CURVE('',#1607,#1605,#1253,.T.);
#1979=EDGE_CURVE('',#1608,#1609,#1254,.T.);
#1980=EDGE_CURVE('',#1609,#1610,#1255,.T.);
#1981=EDGE_CURVE('',#1610,#1608,#1256,.T.);
#1982=EDGE_CURVE('',#1611,#1612,#1257,.T.);
#1983=EDGE_CURVE('',#1612,#1613,#1258,.T.);
#1984=EDGE_CURVE('',#1613,#1611,#1259,.T.);
#1985=EDGE_CURVE('',#1614,#1615,#924,.T.);
#1986=EDGE_CURVE('',#1615,#1616,#1260,.T.);
#1987=EDGE_CURVE('',#1616,#1617,#925,.T.);
#1988=EDGE_CURVE('',#1617,#1618,#1261,.T.);
#1989=EDGE_CURVE('',#1618,#1619,#926,.T.);
#1990=EDGE_CURVE('',#1619,#1620,#1262,.T.);
#1991=EDGE_CURVE('',#1620,#1621,#927,.T.);
#1992=EDGE_CURVE('',#1621,#1614,#1263,.T.);
#1993=EDGE_CURVE('',#1622,#1623,#1264,.T.);
#1994=EDGE_CURVE('',#1623,#1624,#928,.T.);
#1995=EDGE_CURVE('',#1624,#1625,#1265,.T.);
#1996=EDGE_CURVE('',#1625,#1626,#929,.T.);
#1997=EDGE_CURVE('',#1626,#1627,#1266,.T.);
#1998=EDGE_CURVE('',#1627,#1628,#930,.T.);
#1999=EDGE_CURVE('',#1628,#1629,#1267,.T.);
#2000=EDGE_CURVE('',#1629,#1622,#931,.T.);
#2001=EDGE_CURVE('',#1630,#1631,#1268,.T.);
#2002=EDGE_CURVE('',#1631,#1632,#932,.T.);
#2003=EDGE_CURVE('',#1632,#1633,#1269,.T.);
#2004=EDGE_CURVE('',#1633,#1634,#933,.T.);
#2005=EDGE_CURVE('',#1634,#1635,#1270,.T.);
#2006=EDGE_CURVE('',#1635,#1636,#934,.T.);
#2007=EDGE_CURVE('',#1636,#1637,#1271,.T.);
#2008=EDGE_CURVE('',#1637,#1630,#935,.T.);
#2009=EDGE_CURVE('',#1638,#1639,#1272,.T.);
#2010=EDGE_CURVE('',#1639,#1640,#936,.T.);
#2011=EDGE_CURVE('',#1640,#1641,#1273,.T.);
#2012=EDGE_CURVE('',#1641,#1642,#937,.T.);
#2013=EDGE_CURVE('',#1642,#1643,#1274,.T.);
#2014=EDGE_CURVE('',#1643,#1644,#938,.T.);
#2015=EDGE_CURVE('',#1644,#1645,#1275,.T.);
#2016=EDGE_CURVE('',#1645,#1638,#939,.T.);
#2017=EDGE_CURVE('',#1592,#1646,#1276,.T.);
#2018=EDGE_CURVE('',#1646,#1647,#940,.T.);
#2019=EDGE_CURVE('',#1647,#1648,#1277,.T.);
#2020=EDGE_CURVE('',#1648,#1649,#941,.T.);
#2021=EDGE_CURVE('',#1649,#1650,#1278,.T.);
#2022=EDGE_CURVE('',#1650,#1651,#942,.T.);
#2023=EDGE_CURVE('',#1651,#1593,#1279,.T.);
#2024=EDGE_CURVE('',#1652,#1653,#1280,.T.);
#2025=EDGE_CURVE('',#1653,#1654,#943,.T.);
#2026=EDGE_CURVE('',#1654,#1591,#1281,.T.);
#2027=EDGE_CURVE('',#1594,#1655,#1282,.T.);
#2028=EDGE_CURVE('',#1655,#1656,#944,.T.);
#2029=EDGE_CURVE('',#1656,#1657,#1283,.T.);
#2030=EDGE_CURVE('',#1657,#1652,#945,.T.);
#2031=EDGE_CURVE('',#1658,#1659,#1284,.T.);
#2032=EDGE_CURVE('',#1658,#1660,#946,.T.);
#2033=EDGE_CURVE('',#1660,#1661,#1285,.T.);
#2034=EDGE_CURVE('',#1661,#1598,#947,.T.);
#2035=EDGE_CURVE('',#1597,#1662,#948,.T.);
#2036=EDGE_CURVE('',#1662,#1663,#1286,.T.);
#2037=EDGE_CURVE('',#1663,#1664,#949,.T.);
#2038=EDGE_CURVE('',#1664,#1665,#1287,.T.);
#2039=EDGE_CURVE('',#1665,#1666,#950,.T.);
#2040=EDGE_CURVE('',#1666,#1667,#1288,.T.);
#2041=EDGE_CURVE('',#1667,#1659,#951,.T.);
#2042=EDGE_CURVE('',#1668,#1669,#952,.T.);
#2043=EDGE_CURVE('',#1669,#1670,#1289,.T.);
#2044=EDGE_CURVE('',#1670,#1587,#953,.T.);
#2045=EDGE_CURVE('',#1588,#1671,#954,.T.);
#2046=EDGE_CURVE('',#1671,#1672,#1290,.T.);
#2047=EDGE_CURVE('',#1672,#1673,#955,.T.);
#2048=EDGE_CURVE('',#1673,#1674,#1291,.T.);
#2049=EDGE_CURVE('',#1674,#1675,#956,.T.);
#2050=EDGE_CURVE('',#1675,#1676,#1292,.T.);
#2051=EDGE_CURVE('',#1676,#1677,#957,.T.);
#2052=EDGE_CURVE('',#1677,#1668,#1293,.T.);
#2053=EDGE_CURVE('',#1596,#1678,#1294,.T.);
#2054=EDGE_CURVE('',#1678,#1595,#1295,.T.);
#2055=EDGE_CURVE('',#1679,#1680,#1296,.T.);
#2056=EDGE_CURVE('',#1680,#1681,#1297,.T.);
#2057=EDGE_CURVE('',#1681,#1679,#1298,.T.);
#2058=EDGE_CURVE('',#1682,#1683,#1299,.T.);
#2059=EDGE_CURVE('',#1683,#1684,#1300,.T.);
#2060=EDGE_CURVE('',#1684,#1682,#1301,.T.);
#2061=EDGE_CURVE('',#1685,#1686,#1302,.T.);
#2062=EDGE_CURVE('',#1686,#1658,#148,.T.);
#2063=EDGE_CURVE('',#1659,#1687,#149,.T.);
#2064=EDGE_CURVE('',#1687,#1685,#1303,.T.);
#2065=EDGE_CURVE('',#1589,#1688,#1304,.T.);
#2066=EDGE_CURVE('',#1688,#1590,#1305,.T.);
#2067=EDGE_CURVE('',#1689,#1690,#1306,.T.);
#2068=EDGE_CURVE('',#1690,#1691,#1307,.T.);
#2069=EDGE_CURVE('',#1691,#1689,#1308,.T.);
#2070=EDGE_CURVE('',#1692,#1693,#1309,.T.);
#2071=EDGE_CURVE('',#1693,#1694,#1310,.T.);
#2072=EDGE_CURVE('',#1694,#1692,#1311,.T.);
#2073=EDGE_CURVE('',#1695,#1696,#1312,.T.);
#2074=EDGE_CURVE('',#1696,#1697,#1313,.T.);
#2075=EDGE_CURVE('',#1697,#1695,#1314,.T.);
#2076=EDGE_CURVE('',#1640,#1681,#1315,.T.);
#2077=EDGE_CURVE('',#1663,#1640,#1316,.T.);
#2078=EDGE_CURVE('',#1681,#1663,#1317,.T.);
#2079=EDGE_CURVE('',#1664,#1639,#1318,.T.);
#2080=EDGE_CURVE('',#1679,#1662,#1319,.T.);
#2081=EDGE_CURVE('',#1680,#1634,#1320,.T.);
#2082=EDGE_CURVE('',#1635,#1679,#1321,.T.);
#2083=EDGE_CURVE('',#1641,#1680,#1322,.T.);
#2084=EDGE_CURVE('',#1639,#1612,#1323,.T.);
#2085=EDGE_CURVE('',#1613,#1638,#1324,.T.);
#2086=EDGE_CURVE('',#1664,#1612,#1325,.T.);
#2087=EDGE_CURVE('',#1635,#1662,#1326,.T.);
#2088=EDGE_CURVE('',#1641,#1634,#1327,.T.);
#2089=EDGE_CURVE('',#1648,#1638,#1328,.T.);
#2090=EDGE_CURVE('',#1613,#1648,#1329,.T.);
#2091=EDGE_CURVE('',#1611,#1647,#1330,.T.);
#2092=EDGE_CURVE('',#1665,#1611,#1331,.T.);
#2093=EDGE_CURVE('',#1636,#1597,#1332,.T.);
#2094=EDGE_CURVE('',#1642,#1633,#1333,.T.);
#2095=EDGE_CURVE('',#1643,#1690,#1334,.T.);
#2096=EDGE_CURVE('',#1691,#1642,#1335,.T.);
#2097=EDGE_CURVE('',#1644,#1668,#1336,.T.);
#2098=EDGE_CURVE('',#1669,#1643,#1337,.T.);
#2099=EDGE_CURVE('',#1645,#1607,#1338,.T.);
#2100=EDGE_CURVE('',#1605,#1644,#1339,.T.);
#2101=EDGE_CURVE('',#1649,#1645,#1340,.T.);
#2102=EDGE_CURVE('',#1665,#1647,#1341,.T.);
#2103=EDGE_CURVE('',#1636,#1595,#1342,.T.);
#2104=EDGE_CURVE('',#1691,#1633,#1343,.T.);
#2105=EDGE_CURVE('',#1669,#1690,#1344,.T.);
#2106=EDGE_CURVE('',#1605,#1668,#1345,.T.);
#2107=EDGE_CURVE('',#1649,#1607,#1346,.T.);
#2108=EDGE_CURVE('',#1666,#1646,#1347,.T.);
#2109=EDGE_CURVE('',#1678,#1626,#1348,.T.);
#2110=EDGE_CURVE('',#1627,#1596,#1349,.T.);
#2111=EDGE_CURVE('',#1637,#1678,#1350,.T.);
#2112=EDGE_CURVE('',#1689,#1632,#1351,.T.);
#2113=EDGE_CURVE('',#1670,#1689,#1352,.T.);
#2114=EDGE_CURVE('',#1606,#1677,#1353,.T.);
#2115=EDGE_CURVE('',#1650,#1606,#1354,.T.);
#2116=EDGE_CURVE('',#1646,#1682,#1355,.T.);
#2117=EDGE_CURVE('',#1683,#1592,#1356,.T.);
#2118=EDGE_CURVE('',#1666,#1682,#1357,.T.);
#2119=EDGE_CURVE('',#1627,#1598,#1358,.T.);
#2120=EDGE_CURVE('',#1637,#1626,#1359,.T.);
#2121=EDGE_CURVE('',#1670,#1632,#1360,.T.);
#2122=EDGE_CURVE('',#1650,#1677,#1361,.T.);
#2123=EDGE_CURVE('',#1683,#1591,#1362,.T.);
#2124=EDGE_CURVE('',#1684,#1654,#1363,.T.);
#2125=EDGE_CURVE('',#1667,#1684,#1364,.T.);
#2126=EDGE_CURVE('',#1661,#1608,#1365,.T.);
#2127=EDGE_CURVE('',#1609,#1660,#1366,.T.);
#2128=EDGE_CURVE('',#1628,#1661,#1367,.T.);
#2129=EDGE_CURVE('',#1630,#1625,#1368,.T.);
#2130=EDGE_CURVE('',#1631,#1589,#1369,.T.);
#2131=EDGE_CURVE('',#1688,#1630,#1370,.T.);
#2132=EDGE_CURVE('',#1587,#1631,#1371,.T.);
#2133=EDGE_CURVE('',#1651,#1676,#1372,.T.);
#2134=EDGE_CURVE('',#1593,#1694,#1373,.T.);
#2135=EDGE_CURVE('',#1692,#1651,#1374,.T.);
#2136=EDGE_CURVE('',#1667,#1654,#1375,.T.);
#2137=EDGE_CURVE('',#1609,#1620,#1376,.T.);
#2138=EDGE_CURVE('',#1620,#1660,#1377,.T.);
#2139=EDGE_CURVE('',#1628,#1608,#1378,.T.);
#2140=EDGE_CURVE('',#1688,#1625,#1379,.T.);
#2141=EDGE_CURVE('',#1692,#1676,#1380,.T.);
#2142=EDGE_CURVE('',#1594,#1694,#1381,.T.);
#2143=EDGE_CURVE('',#1687,#1653,#1382,.T.);
#2144=EDGE_CURVE('',#1621,#1686,#1383,.T.);
#2145=EDGE_CURVE('',#1610,#1619,#1384,.T.);
#2146=EDGE_CURVE('',#1629,#1610,#1385,.T.);
#2147=EDGE_CURVE('',#1590,#1624,#1386,.T.);
#2148=EDGE_CURVE('',#1693,#1675,#1387,.T.);
#2149=EDGE_CURVE('',#1655,#1693,#1388,.T.);
#2150=EDGE_CURVE('',#1685,#1652,#1389,.T.);
#2151=EDGE_CURVE('',#1614,#1685,#1390,.T.);
#2152=EDGE_CURVE('',#1629,#1619,#1391,.T.);
#2153=EDGE_CURVE('',#1588,#1624,#1392,.T.);
#2154=EDGE_CURVE('',#1655,#1675,#1393,.T.);
#2155=EDGE_CURVE('',#1614,#1652,#1394,.T.);
#2156=EDGE_CURVE('',#1622,#1618,#1395,.T.);
#2157=EDGE_CURVE('',#1623,#1603,#1396,.T.);
#2158=EDGE_CURVE('',#1604,#1622,#1397,.T.);
#2159=EDGE_CURVE('',#1671,#1623,#1398,.T.);
#2160=EDGE_CURVE('',#1656,#1674,#1399,.T.);
#2161=EDGE_CURVE('',#1657,#1697,#1400,.T.);
#2162=EDGE_CURVE('',#1695,#1656,#1401,.T.);
#2163=EDGE_CURVE('',#1615,#1657,#1402,.T.);
#2164=EDGE_CURVE('',#1604,#1618,#1403,.T.);
#2165=EDGE_CURVE('',#1671,#1603,#1404,.T.);
#2166=EDGE_CURVE('',#1695,#1674,#1405,.T.);
#2167=EDGE_CURVE('',#1615,#1697,#1406,.T.);
#2168=EDGE_CURVE('',#1602,#1617,#1407,.T.);
#2169=EDGE_CURVE('',#1672,#1602,#1408,.T.);
#2170=EDGE_CURVE('',#1696,#1673,#1409,.T.);
#2171=EDGE_CURVE('',#1616,#1696,#1410,.T.);
#2172=EDGE_CURVE('',#1672,#1617,#1411,.T.);
#2173=EDGE_CURVE('',#1616,#1673,#1412,.T.);
#2678=ORIENTED_EDGE('',*,*,#1952,.F.);
#2679=ORIENTED_EDGE('',*,*,#1953,.T.);
#2680=ORIENTED_EDGE('',*,*,#1954,.F.);
#2681=ORIENTED_EDGE('',*,*,#1953,.F.);
#2682=ORIENTED_EDGE('',*,*,#1955,.F.);
#2683=ORIENTED_EDGE('',*,*,#1956,.T.);
#2684=ORIENTED_EDGE('',*,*,#1952,.T.);
#2685=ORIENTED_EDGE('',*,*,#1956,.F.);
#2686=ORIENTED_EDGE('',*,*,#1957,.F.);
#2687=ORIENTED_EDGE('',*,*,#1958,.T.);
#2688=ORIENTED_EDGE('',*,*,#1959,.F.);
#2689=ORIENTED_EDGE('',*,*,#1960,.F.);
#2690=ORIENTED_EDGE('',*,*,#1961,.T.);
#2691=ORIENTED_EDGE('',*,*,#1962,.F.);
#2692=ORIENTED_EDGE('',*,*,#1963,.F.);
#2693=ORIENTED_EDGE('',*,*,#1964,.F.);
#2694=ORIENTED_EDGE('',*,*,#1965,.F.);
#2695=ORIENTED_EDGE('',*,*,#1966,.T.);
#2696=ORIENTED_EDGE('',*,*,#1967,.F.);
#2697=ORIENTED_EDGE('',*,*,#1968,.F.);
#2698=ORIENTED_EDGE('',*,*,#1969,.F.);
#2699=ORIENTED_EDGE('',*,*,#1970,.F.);
#2700=ORIENTED_EDGE('',*,*,#1970,.T.);
#2701=ORIENTED_EDGE('',*,*,#1971,.T.);
#2702=ORIENTED_EDGE('',*,*,#1972,.T.);
#2703=ORIENTED_EDGE('',*,*,#1969,.T.);
#2704=ORIENTED_EDGE('',*,*,#1972,.F.);
#2705=ORIENTED_EDGE('',*,*,#1973,.T.);
#2706=ORIENTED_EDGE('',*,*,#1974,.T.);
#2707=ORIENTED_EDGE('',*,*,#1975,.T.);
#2708=ORIENTED_EDGE('',*,*,#1976,.T.);
#2709=ORIENTED_EDGE('',*,*,#1977,.T.);
#2710=ORIENTED_EDGE('',*,*,#1978,.T.);
#2711=ORIENTED_EDGE('',*,*,#1979,.T.);
#2712=ORIENTED_EDGE('',*,*,#1980,.T.);
#2713=ORIENTED_EDGE('',*,*,#1981,.T.);
#2714=ORIENTED_EDGE('',*,*,#1982,.T.);
#2715=ORIENTED_EDGE('',*,*,#1983,.T.);
#2716=ORIENTED_EDGE('',*,*,#1984,.T.);
#2717=ORIENTED_EDGE('',*,*,#1985,.T.);
#2718=ORIENTED_EDGE('',*,*,#1986,.T.);
#2719=ORIENTED_EDGE('',*,*,#1987,.T.);
#2720=ORIENTED_EDGE('',*,*,#1988,.T.);
#2721=ORIENTED_EDGE('',*,*,#1989,.T.);
#2722=ORIENTED_EDGE('',*,*,#1990,.T.);
#2723=ORIENTED_EDGE('',*,*,#1991,.T.);
#2724=ORIENTED_EDGE('',*,*,#1992,.T.);
#2725=ORIENTED_EDGE('',*,*,#1993,.T.);
#2726=ORIENTED_EDGE('',*,*,#1994,.T.);
#2727=ORIENTED_EDGE('',*,*,#1995,.T.);
#2728=ORIENTED_EDGE('',*,*,#1996,.T.);
#2729=ORIENTED_EDGE('',*,*,#1997,.T.);
#2730=ORIENTED_EDGE('',*,*,#1998,.T.);
#2731=ORIENTED_EDGE('',*,*,#1999,.T.);
#2732=ORIENTED_EDGE('',*,*,#2000,.T.);
#2733=ORIENTED_EDGE('',*,*,#2001,.T.);
#2734=ORIENTED_EDGE('',*,*,#2002,.T.);
#2735=ORIENTED_EDGE('',*,*,#2003,.T.);
#2736=ORIENTED_EDGE('',*,*,#2004,.T.);
#2737=ORIENTED_EDGE('',*,*,#2005,.T.);
#2738=ORIENTED_EDGE('',*,*,#2006,.T.);
#2739=ORIENTED_EDGE('',*,*,#2007,.T.);
#2740=ORIENTED_EDGE('',*,*,#2008,.T.);
#2741=ORIENTED_EDGE('',*,*,#2009,.T.);
#2742=ORIENTED_EDGE('',*,*,#2010,.T.);
#2743=ORIENTED_EDGE('',*,*,#2011,.T.);
#2744=ORIENTED_EDGE('',*,*,#2012,.T.);
#2745=ORIENTED_EDGE('',*,*,#2013,.T.);
#2746=ORIENTED_EDGE('',*,*,#2014,.T.);
#2747=ORIENTED_EDGE('',*,*,#2015,.T.);
#2748=ORIENTED_EDGE('',*,*,#2016,.T.);
#2749=ORIENTED_EDGE('',*,*,#2017,.T.);
#2750=ORIENTED_EDGE('',*,*,#2018,.T.);
#2751=ORIENTED_EDGE('',*,*,#2019,.T.);
#2752=ORIENTED_EDGE('',*,*,#2020,.T.);
#2753=ORIENTED_EDGE('',*,*,#2021,.T.);
#2754=ORIENTED_EDGE('',*,*,#2022,.T.);
#2755=ORIENTED_EDGE('',*,*,#2023,.T.);
#2756=ORIENTED_EDGE('',*,*,#1962,.T.);
#2757=ORIENTED_EDGE('',*,*,#2024,.T.);
#2758=ORIENTED_EDGE('',*,*,#2025,.T.);
#2759=ORIENTED_EDGE('',*,*,#2026,.T.);
#2760=ORIENTED_EDGE('',*,*,#1964,.T.);
#2761=ORIENTED_EDGE('',*,*,#2027,.T.);
#2762=ORIENTED_EDGE('',*,*,#2028,.T.);
#2763=ORIENTED_EDGE('',*,*,#2029,.T.);
#2764=ORIENTED_EDGE('',*,*,#2030,.T.);
#2765=ORIENTED_EDGE('',*,*,#2031,.F.);
#2766=ORIENTED_EDGE('',*,*,#2032,.T.);
#2767=ORIENTED_EDGE('',*,*,#2033,.T.);
#2768=ORIENTED_EDGE('',*,*,#2034,.T.);
#2769=ORIENTED_EDGE('',*,*,#1967,.T.);
#2770=ORIENTED_EDGE('',*,*,#2035,.T.);
#2771=ORIENTED_EDGE('',*,*,#2036,.T.);
#2772=ORIENTED_EDGE('',*,*,#2037,.T.);
#2773=ORIENTED_EDGE('',*,*,#2038,.T.);
#2774=ORIENTED_EDGE('',*,*,#2039,.T.);
#2775=ORIENTED_EDGE('',*,*,#2040,.T.);
#2776=ORIENTED_EDGE('',*,*,#2041,.T.);
#2777=ORIENTED_EDGE('',*,*,#1971,.F.);
#2778=ORIENTED_EDGE('',*,*,#2042,.T.);
#2779=ORIENTED_EDGE('',*,*,#2043,.T.);
#2780=ORIENTED_EDGE('',*,*,#2044,.T.);
#2781=ORIENTED_EDGE('',*,*,#1957,.T.);
#2782=ORIENTED_EDGE('',*,*,#2045,.T.);
#2783=ORIENTED_EDGE('',*,*,#2046,.T.);
#2784=ORIENTED_EDGE('',*,*,#2047,.T.);
#2785=ORIENTED_EDGE('',*,*,#2048,.T.);
#2786=ORIENTED_EDGE('',*,*,#2049,.T.);
#2787=ORIENTED_EDGE('',*,*,#2050,.T.);
#2788=ORIENTED_EDGE('',*,*,#2051,.T.);
#2789=ORIENTED_EDGE('',*,*,#2052,.T.);
#2790=ORIENTED_EDGE('',*,*,#1954,.T.);
#2791=ORIENTED_EDGE('',*,*,#1965,.T.);
#2792=ORIENTED_EDGE('',*,*,#2053,.T.);
#2793=ORIENTED_EDGE('',*,*,#2054,.T.);
#2794=ORIENTED_EDGE('',*,*,#2055,.T.);
#2795=ORIENTED_EDGE('',*,*,#2056,.T.);
#2796=ORIENTED_EDGE('',*,*,#2057,.T.);
#2797=ORIENTED_EDGE('',*,*,#2058,.T.);
#2798=ORIENTED_EDGE('',*,*,#2059,.T.);
#2799=ORIENTED_EDGE('',*,*,#2060,.T.);
#2800=ORIENTED_EDGE('',*,*,#2061,.T.);
#2801=ORIENTED_EDGE('',*,*,#2062,.T.);
#2802=ORIENTED_EDGE('',*,*,#2031,.T.);
#2803=ORIENTED_EDGE('',*,*,#2063,.T.);
#2804=ORIENTED_EDGE('',*,*,#2064,.T.);
#2805=ORIENTED_EDGE('',*,*,#2065,.T.);
#2806=ORIENTED_EDGE('',*,*,#2066,.T.);
#2807=ORIENTED_EDGE('',*,*,#1959,.T.);
#2808=ORIENTED_EDGE('',*,*,#2067,.T.);
#2809=ORIENTED_EDGE('',*,*,#2068,.T.);
#2810=ORIENTED_EDGE('',*,*,#2069,.T.);
#2811=ORIENTED_EDGE('',*,*,#2070,.T.);
#2812=ORIENTED_EDGE('',*,*,#2071,.T.);
#2813=ORIENTED_EDGE('',*,*,#2072,.T.);
#2814=ORIENTED_EDGE('',*,*,#2073,.T.);
#2815=ORIENTED_EDGE('',*,*,#2074,.T.);
#2816=ORIENTED_EDGE('',*,*,#2075,.T.);
#2817=ORIENTED_EDGE('',*,*,#2076,.F.);
#2818=ORIENTED_EDGE('',*,*,#2077,.F.);
#2819=ORIENTED_EDGE('',*,*,#2078,.F.);
#2820=ORIENTED_EDGE('',*,*,#2077,.T.);
#2821=ORIENTED_EDGE('',*,*,#2010,.F.);
#2822=ORIENTED_EDGE('',*,*,#2079,.F.);
#2823=ORIENTED_EDGE('',*,*,#2037,.F.);
#2824=ORIENTED_EDGE('',*,*,#2078,.T.);
#2825=ORIENTED_EDGE('',*,*,#2036,.F.);
#2826=ORIENTED_EDGE('',*,*,#2080,.F.);
#2827=ORIENTED_EDGE('',*,*,#2057,.F.);
#2828=ORIENTED_EDGE('',*,*,#2081,.F.);
#2829=ORIENTED_EDGE('',*,*,#2055,.F.);
#2830=ORIENTED_EDGE('',*,*,#2082,.F.);
#2831=ORIENTED_EDGE('',*,*,#2005,.F.);
#2832=ORIENTED_EDGE('',*,*,#2076,.T.);
#2833=ORIENTED_EDGE('',*,*,#2056,.F.);
#2834=ORIENTED_EDGE('',*,*,#2083,.F.);
#2835=ORIENTED_EDGE('',*,*,#2011,.F.);
#2836=ORIENTED_EDGE('',*,*,#2084,.F.);
#2837=ORIENTED_EDGE('',*,*,#2009,.F.);
#2838=ORIENTED_EDGE('',*,*,#2085,.F.);
#2839=ORIENTED_EDGE('',*,*,#1983,.F.);
#2840=ORIENTED_EDGE('',*,*,#2079,.T.);
#2841=ORIENTED_EDGE('',*,*,#2084,.T.);
#2842=ORIENTED_EDGE('',*,*,#2086,.F.);
#2843=ORIENTED_EDGE('',*,*,#2082,.T.);
#2844=ORIENTED_EDGE('',*,*,#2080,.T.);
#2845=ORIENTED_EDGE('',*,*,#2087,.F.);
#2846=ORIENTED_EDGE('',*,*,#2083,.T.);
#2847=ORIENTED_EDGE('',*,*,#2081,.T.);
#2848=ORIENTED_EDGE('',*,*,#2088,.F.);
#2849=ORIENTED_EDGE('',*,*,#2089,.F.);
#2850=ORIENTED_EDGE('',*,*,#2090,.F.);
#2851=ORIENTED_EDGE('',*,*,#2085,.T.);
#2852=ORIENTED_EDGE('',*,*,#2090,.T.);
#2853=ORIENTED_EDGE('',*,*,#2019,.F.);
#2854=ORIENTED_EDGE('',*,*,#2091,.F.);
#2855=ORIENTED_EDGE('',*,*,#1984,.F.);
#2856=ORIENTED_EDGE('',*,*,#2086,.T.);
#2857=ORIENTED_EDGE('',*,*,#1982,.F.);
#2858=ORIENTED_EDGE('',*,*,#2092,.F.);
#2859=ORIENTED_EDGE('',*,*,#2038,.F.);
#2860=ORIENTED_EDGE('',*,*,#2087,.T.);
#2861=ORIENTED_EDGE('',*,*,#2035,.F.);
#2862=ORIENTED_EDGE('',*,*,#2093,.F.);
#2863=ORIENTED_EDGE('',*,*,#2006,.F.);
#2864=ORIENTED_EDGE('',*,*,#2088,.T.);
#2865=ORIENTED_EDGE('',*,*,#2004,.F.);
#2866=ORIENTED_EDGE('',*,*,#2094,.F.);
#2867=ORIENTED_EDGE('',*,*,#2012,.F.);
#2868=ORIENTED_EDGE('',*,*,#2095,.F.);
#2869=ORIENTED_EDGE('',*,*,#2013,.F.);
#2870=ORIENTED_EDGE('',*,*,#2096,.F.);
#2871=ORIENTED_EDGE('',*,*,#2068,.F.);
#2872=ORIENTED_EDGE('',*,*,#2097,.F.);
#2873=ORIENTED_EDGE('',*,*,#2014,.F.);
#2874=ORIENTED_EDGE('',*,*,#2098,.F.);
#2875=ORIENTED_EDGE('',*,*,#2042,.F.);
#2876=ORIENTED_EDGE('',*,*,#2099,.F.);
#2877=ORIENTED_EDGE('',*,*,#2015,.F.);
#2878=ORIENTED_EDGE('',*,*,#2100,.F.);
#2879=ORIENTED_EDGE('',*,*,#1978,.F.);
#2880=ORIENTED_EDGE('',*,*,#2089,.T.);
#2881=ORIENTED_EDGE('',*,*,#2016,.F.);
#2882=ORIENTED_EDGE('',*,*,#2101,.F.);
#2883=ORIENTED_EDGE('',*,*,#2020,.F.);
#2884=ORIENTED_EDGE('',*,*,#2092,.T.);
#2885=ORIENTED_EDGE('',*,*,#2091,.T.);
#2886=ORIENTED_EDGE('',*,*,#2102,.F.);
#2887=ORIENTED_EDGE('',*,*,#2103,.F.);
#2888=ORIENTED_EDGE('',*,*,#2093,.T.);
#2889=ORIENTED_EDGE('',*,*,#1966,.F.);
#2890=ORIENTED_EDGE('',*,*,#2096,.T.);
#2891=ORIENTED_EDGE('',*,*,#2094,.T.);
#2892=ORIENTED_EDGE('',*,*,#2104,.F.);
#2893=ORIENTED_EDGE('',*,*,#2098,.T.);
#2894=ORIENTED_EDGE('',*,*,#2095,.T.);
#2895=ORIENTED_EDGE('',*,*,#2105,.F.);
#2896=ORIENTED_EDGE('',*,*,#2100,.T.);
#2897=ORIENTED_EDGE('',*,*,#2097,.T.);
#2898=ORIENTED_EDGE('',*,*,#2106,.F.);
#2899=ORIENTED_EDGE('',*,*,#2101,.T.);
#2900=ORIENTED_EDGE('',*,*,#2099,.T.);
#2901=ORIENTED_EDGE('',*,*,#2107,.F.);
#2902=ORIENTED_EDGE('',*,*,#2102,.T.);
#2903=ORIENTED_EDGE('',*,*,#2018,.F.);
#2904=ORIENTED_EDGE('',*,*,#2108,.F.);
#2905=ORIENTED_EDGE('',*,*,#2039,.F.);
#2906=ORIENTED_EDGE('',*,*,#2109,.F.);
#2907=ORIENTED_EDGE('',*,*,#2053,.F.);
#2908=ORIENTED_EDGE('',*,*,#2110,.F.);
#2909=ORIENTED_EDGE('',*,*,#1997,.F.);
#2910=ORIENTED_EDGE('',*,*,#2103,.T.);
#2911=ORIENTED_EDGE('',*,*,#2054,.F.);
#2912=ORIENTED_EDGE('',*,*,#2111,.F.);
#2913=ORIENTED_EDGE('',*,*,#2007,.F.);
#2914=ORIENTED_EDGE('',*,*,#2104,.T.);
#2915=ORIENTED_EDGE('',*,*,#2003,.F.);
#2916=ORIENTED_EDGE('',*,*,#2112,.F.);
#2917=ORIENTED_EDGE('',*,*,#2069,.F.);
#2918=ORIENTED_EDGE('',*,*,#2105,.T.);
#2919=ORIENTED_EDGE('',*,*,#2067,.F.);
#2920=ORIENTED_EDGE('',*,*,#2113,.F.);
#2921=ORIENTED_EDGE('',*,*,#2043,.F.);
#2922=ORIENTED_EDGE('',*,*,#2106,.T.);
#2923=ORIENTED_EDGE('',*,*,#2052,.F.);
#2924=ORIENTED_EDGE('',*,*,#2114,.F.);
#2925=ORIENTED_EDGE('',*,*,#1976,.F.);
#2926=ORIENTED_EDGE('',*,*,#2107,.T.);
#2927=ORIENTED_EDGE('',*,*,#1977,.F.);
#2928=ORIENTED_EDGE('',*,*,#2115,.F.);
#2929=ORIENTED_EDGE('',*,*,#2021,.F.);
#2930=ORIENTED_EDGE('',*,*,#2116,.F.);
#2931=ORIENTED_EDGE('',*,*,#2017,.F.);
#2932=ORIENTED_EDGE('',*,*,#2117,.F.);
#2933=ORIENTED_EDGE('',*,*,#2058,.F.);
#2934=ORIENTED_EDGE('',*,*,#2108,.T.);
#2935=ORIENTED_EDGE('',*,*,#2116,.T.);
#2936=ORIENTED_EDGE('',*,*,#2118,.F.);
#2937=ORIENTED_EDGE('',*,*,#2110,.T.);
#2938=ORIENTED_EDGE('',*,*,#1968,.T.);
#2939=ORIENTED_EDGE('',*,*,#2119,.F.);
#2940=ORIENTED_EDGE('',*,*,#2111,.T.);
#2941=ORIENTED_EDGE('',*,*,#2109,.T.);
#2942=ORIENTED_EDGE('',*,*,#2120,.F.);
#2943=ORIENTED_EDGE('',*,*,#2113,.T.);
#2944=ORIENTED_EDGE('',*,*,#2112,.T.);
#2945=ORIENTED_EDGE('',*,*,#2121,.F.);
#2946=ORIENTED_EDGE('',*,*,#2115,.T.);
#2947=ORIENTED_EDGE('',*,*,#2114,.T.);
#2948=ORIENTED_EDGE('',*,*,#2122,.F.);
#2949=ORIENTED_EDGE('',*,*,#1961,.F.);
#2950=ORIENTED_EDGE('',*,*,#2123,.F.);
#2951=ORIENTED_EDGE('',*,*,#2117,.T.);
#2952=ORIENTED_EDGE('',*,*,#2123,.T.);
#2953=ORIENTED_EDGE('',*,*,#2026,.F.);
#2954=ORIENTED_EDGE('',*,*,#2124,.F.);
#2955=ORIENTED_EDGE('',*,*,#2059,.F.);
#2956=ORIENTED_EDGE('',*,*,#2118,.T.);
#2957=ORIENTED_EDGE('',*,*,#2060,.F.);
#2958=ORIENTED_EDGE('',*,*,#2125,.F.);
#2959=ORIENTED_EDGE('',*,*,#2040,.F.);
#2960=ORIENTED_EDGE('',*,*,#2126,.F.);
#2961=ORIENTED_EDGE('',*,*,#2033,.F.);
#2962=ORIENTED_EDGE('',*,*,#2127,.F.);
#2963=ORIENTED_EDGE('',*,*,#1979,.F.);
#2964=ORIENTED_EDGE('',*,*,#2119,.T.);
#2965=ORIENTED_EDGE('',*,*,#2034,.F.);
#2966=ORIENTED_EDGE('',*,*,#2128,.F.);
#2967=ORIENTED_EDGE('',*,*,#1998,.F.);
#2968=ORIENTED_EDGE('',*,*,#2120,.T.);
#2969=ORIENTED_EDGE('',*,*,#1996,.F.);
#2970=ORIENTED_EDGE('',*,*,#2129,.F.);
#2971=ORIENTED_EDGE('',*,*,#2008,.F.);
#2972=ORIENTED_EDGE('',*,*,#2130,.F.);
#2973=ORIENTED_EDGE('',*,*,#2001,.F.);
#2974=ORIENTED_EDGE('',*,*,#2131,.F.);
#2975=ORIENTED_EDGE('',*,*,#2065,.F.);
#2976=ORIENTED_EDGE('',*,*,#2121,.T.);
#2977=ORIENTED_EDGE('',*,*,#2002,.F.);
#2978=ORIENTED_EDGE('',*,*,#2132,.F.);
#2979=ORIENTED_EDGE('',*,*,#2044,.F.);
#2980=ORIENTED_EDGE('',*,*,#2122,.T.);
#2981=ORIENTED_EDGE('',*,*,#2051,.F.);
#2982=ORIENTED_EDGE('',*,*,#2133,.F.);
#2983=ORIENTED_EDGE('',*,*,#2022,.F.);
#2984=ORIENTED_EDGE('',*,*,#2134,.F.);
#2985=ORIENTED_EDGE('',*,*,#2023,.F.);
#2986=ORIENTED_EDGE('',*,*,#2135,.F.);
#2987=ORIENTED_EDGE('',*,*,#2072,.F.);
#2988=ORIENTED_EDGE('',*,*,#2125,.T.);
#2989=ORIENTED_EDGE('',*,*,#2124,.T.);
#2990=ORIENTED_EDGE('',*,*,#2136,.F.);
#2991=ORIENTED_EDGE('',*,*,#2137,.F.);
#2992=ORIENTED_EDGE('',*,*,#2127,.T.);
#2993=ORIENTED_EDGE('',*,*,#2138,.F.);
#2994=ORIENTED_EDGE('',*,*,#2128,.T.);
#2995=ORIENTED_EDGE('',*,*,#2126,.T.);
#2996=ORIENTED_EDGE('',*,*,#2139,.F.);
#2997=ORIENTED_EDGE('',*,*,#2131,.T.);
#2998=ORIENTED_EDGE('',*,*,#2129,.T.);
#2999=ORIENTED_EDGE('',*,*,#2140,.F.);
#3000=ORIENTED_EDGE('',*,*,#2132,.T.);
#3001=ORIENTED_EDGE('',*,*,#2130,.T.);
#3002=ORIENTED_EDGE('',*,*,#1958,.F.);
#3003=ORIENTED_EDGE('',*,*,#2135,.T.);
#3004=ORIENTED_EDGE('',*,*,#2133,.T.);
#3005=ORIENTED_EDGE('',*,*,#2141,.F.);
#3006=ORIENTED_EDGE('',*,*,#1963,.T.);
#3007=ORIENTED_EDGE('',*,*,#2134,.T.);
#3008=ORIENTED_EDGE('',*,*,#2142,.F.);
#3009=ORIENTED_EDGE('',*,*,#2136,.T.);
#3010=ORIENTED_EDGE('',*,*,#2025,.F.);
#3011=ORIENTED_EDGE('',*,*,#2143,.F.);
#3012=ORIENTED_EDGE('',*,*,#2063,.F.);
#3013=ORIENTED_EDGE('',*,*,#2041,.F.);
#3014=ORIENTED_EDGE('',*,*,#2032,.F.);
#3015=ORIENTED_EDGE('',*,*,#2062,.F.);
#3016=ORIENTED_EDGE('',*,*,#2144,.F.);
#3017=ORIENTED_EDGE('',*,*,#1991,.F.);
#3018=ORIENTED_EDGE('',*,*,#2138,.T.);
#3019=ORIENTED_EDGE('',*,*,#2137,.T.);
#3020=ORIENTED_EDGE('',*,*,#1990,.F.);
#3021=ORIENTED_EDGE('',*,*,#2145,.F.);
#3022=ORIENTED_EDGE('',*,*,#1980,.F.);
#3023=ORIENTED_EDGE('',*,*,#2139,.T.);
#3024=ORIENTED_EDGE('',*,*,#1981,.F.);
#3025=ORIENTED_EDGE('',*,*,#2146,.F.);
#3026=ORIENTED_EDGE('',*,*,#1999,.F.);
#3027=ORIENTED_EDGE('',*,*,#2140,.T.);
#3028=ORIENTED_EDGE('',*,*,#1995,.F.);
#3029=ORIENTED_EDGE('',*,*,#2147,.F.);
#3030=ORIENTED_EDGE('',*,*,#2066,.F.);
#3031=ORIENTED_EDGE('',*,*,#2141,.T.);
#3032=ORIENTED_EDGE('',*,*,#2050,.F.);
#3033=ORIENTED_EDGE('',*,*,#2148,.F.);
#3034=ORIENTED_EDGE('',*,*,#2070,.F.);
#3035=ORIENTED_EDGE('',*,*,#2142,.T.);
#3036=ORIENTED_EDGE('',*,*,#2071,.F.);
#3037=ORIENTED_EDGE('',*,*,#2149,.F.);
#3038=ORIENTED_EDGE('',*,*,#2027,.F.);
#3039=ORIENTED_EDGE('',*,*,#2143,.T.);
#3040=ORIENTED_EDGE('',*,*,#2024,.F.);
#3041=ORIENTED_EDGE('',*,*,#2150,.F.);
#3042=ORIENTED_EDGE('',*,*,#2064,.F.);
#3043=ORIENTED_EDGE('',*,*,#2144,.T.);
#3044=ORIENTED_EDGE('',*,*,#2061,.F.);
#3045=ORIENTED_EDGE('',*,*,#2151,.F.);
#3046=ORIENTED_EDGE('',*,*,#1992,.F.);
#3047=ORIENTED_EDGE('',*,*,#2146,.T.);
#3048=ORIENTED_EDGE('',*,*,#2145,.T.);
#3049=ORIENTED_EDGE('',*,*,#2152,.F.);
#3050=ORIENTED_EDGE('',*,*,#1960,.T.);
#3051=ORIENTED_EDGE('',*,*,#2147,.T.);
#3052=ORIENTED_EDGE('',*,*,#2153,.F.);
#3053=ORIENTED_EDGE('',*,*,#2149,.T.);
#3054=ORIENTED_EDGE('',*,*,#2148,.T.);
#3055=ORIENTED_EDGE('',*,*,#2154,.F.);
#3056=ORIENTED_EDGE('',*,*,#2151,.T.);
#3057=ORIENTED_EDGE('',*,*,#2150,.T.);
#3058=ORIENTED_EDGE('',*,*,#2155,.F.);
#3059=ORIENTED_EDGE('',*,*,#2152,.T.);
#3060=ORIENTED_EDGE('',*,*,#1989,.F.);
#3061=ORIENTED_EDGE('',*,*,#2156,.F.);
#3062=ORIENTED_EDGE('',*,*,#2000,.F.);
#3063=ORIENTED_EDGE('',*,*,#2157,.F.);
#3064=ORIENTED_EDGE('',*,*,#1993,.F.);
#3065=ORIENTED_EDGE('',*,*,#2158,.F.);
#3066=ORIENTED_EDGE('',*,*,#1974,.F.);
#3067=ORIENTED_EDGE('',*,*,#2153,.T.);
#3068=ORIENTED_EDGE('',*,*,#1994,.F.);
#3069=ORIENTED_EDGE('',*,*,#2159,.F.);
#3070=ORIENTED_EDGE('',*,*,#2045,.F.);
#3071=ORIENTED_EDGE('',*,*,#2154,.T.);
#3072=ORIENTED_EDGE('',*,*,#2049,.F.);
#3073=ORIENTED_EDGE('',*,*,#2160,.F.);
#3074=ORIENTED_EDGE('',*,*,#2028,.F.);
#3075=ORIENTED_EDGE('',*,*,#2161,.F.);
#3076=ORIENTED_EDGE('',*,*,#2029,.F.);
#3077=ORIENTED_EDGE('',*,*,#2162,.F.);
#3078=ORIENTED_EDGE('',*,*,#2075,.F.);
#3079=ORIENTED_EDGE('',*,*,#2155,.T.);
#3080=ORIENTED_EDGE('',*,*,#2030,.F.);
#3081=ORIENTED_EDGE('',*,*,#2163,.F.);
#3082=ORIENTED_EDGE('',*,*,#1985,.F.);
#3083=ORIENTED_EDGE('',*,*,#2158,.T.);
#3084=ORIENTED_EDGE('',*,*,#2156,.T.);
#3085=ORIENTED_EDGE('',*,*,#2164,.F.);
#3086=ORIENTED_EDGE('',*,*,#2159,.T.);
#3087=ORIENTED_EDGE('',*,*,#2157,.T.);
#3088=ORIENTED_EDGE('',*,*,#2165,.F.);
#3089=ORIENTED_EDGE('',*,*,#2162,.T.);
#3090=ORIENTED_EDGE('',*,*,#2160,.T.);
#3091=ORIENTED_EDGE('',*,*,#2166,.F.);
#3092=ORIENTED_EDGE('',*,*,#2163,.T.);
#3093=ORIENTED_EDGE('',*,*,#2161,.T.);
#3094=ORIENTED_EDGE('',*,*,#2167,.F.);
#3095=ORIENTED_EDGE('',*,*,#2164,.T.);
#3096=ORIENTED_EDGE('',*,*,#1988,.F.);
#3097=ORIENTED_EDGE('',*,*,#2168,.F.);
#3098=ORIENTED_EDGE('',*,*,#1975,.F.);
#3099=ORIENTED_EDGE('',*,*,#2165,.T.);
#3100=ORIENTED_EDGE('',*,*,#1973,.F.);
#3101=ORIENTED_EDGE('',*,*,#2169,.F.);
#3102=ORIENTED_EDGE('',*,*,#2046,.F.);
#3103=ORIENTED_EDGE('',*,*,#2166,.T.);
#3104=ORIENTED_EDGE('',*,*,#2048,.F.);
#3105=ORIENTED_EDGE('',*,*,#2170,.F.);
#3106=ORIENTED_EDGE('',*,*,#2073,.F.);
#3107=ORIENTED_EDGE('',*,*,#2167,.T.);
#3108=ORIENTED_EDGE('',*,*,#2074,.F.);
#3109=ORIENTED_EDGE('',*,*,#2171,.F.);
#3110=ORIENTED_EDGE('',*,*,#1986,.F.);
#3111=ORIENTED_EDGE('',*,*,#2169,.T.);
#3112=ORIENTED_EDGE('',*,*,#2168,.T.);
#3113=ORIENTED_EDGE('',*,*,#2172,.F.);
#3114=ORIENTED_EDGE('',*,*,#2171,.T.);
#3115=ORIENTED_EDGE('',*,*,#2170,.T.);
#3116=ORIENTED_EDGE('',*,*,#2173,.F.);
#3117=ORIENTED_EDGE('',*,*,#2172,.T.);
#3118=ORIENTED_EDGE('',*,*,#1987,.F.);
#3119=ORIENTED_EDGE('',*,*,#2173,.T.);
#3120=ORIENTED_EDGE('',*,*,#2047,.F.);
#3121=ORIENTED_EDGE('',*,*,#1955,.T.);
#3186=CYLINDRICAL_SURFACE('',#3722,1.15);
#3187=CYLINDRICAL_SURFACE('',#3729,0.0500000000000001);
#3188=CYLINDRICAL_SURFACE('',#3740,2.525);
#3189=CYLINDRICAL_SURFACE('',#3833,0.0500000000000001);
#3190=CYLINDRICAL_SURFACE('',#3858,0.0500000000000001);
#3191=CYLINDRICAL_SURFACE('',#3860,0.0499999999999999);
#3192=CYLINDRICAL_SURFACE('',#3865,0.0500000000000001);
#3193=CYLINDRICAL_SURFACE('',#3871,0.0499999999999999);
#3194=CYLINDRICAL_SURFACE('',#3885,0.0500000000000002);
#3195=CYLINDRICAL_SURFACE('',#3922,0.0500000000000001);
#3196=CYLINDRICAL_SURFACE('',#3924,0.0500000000000001);
#3197=CYLINDRICAL_SURFACE('',#3929,0.0500000000000001);
#3198=CYLINDRICAL_SURFACE('',#3931,0.0500000000000002);
#3199=CYLINDRICAL_SURFACE('',#3950,0.0500000000000001);
#3200=CYLINDRICAL_SURFACE('',#3952,0.0500000000000001);
#3201=CYLINDRICAL_SURFACE('',#3976,0.0499999999999999);
#3202=CYLINDRICAL_SURFACE('',#3981,0.0500000000000001);
#3203=CYLINDRICAL_SURFACE('',#3983,0.0500000000000001);
#3204=CYLINDRICAL_SURFACE('',#3988,0.0499999999999999);
#3205=CYLINDRICAL_SURFACE('',#4010,0.0500000000000001);
#3308=ADVANCED_FACE('',(#396),#137,.F.);
#3309=ADVANCED_FACE('',(#397),#3186,.F.);
#3310=ADVANCED_FACE('',(#398),#97,.T.);
#3311=ADVANCED_FACE('',(#399),#3187,.T.);
#3312=ADVANCED_FACE('',(#400),#98,.T.);
#3313=ADVANCED_FACE('',(#401),#50,.T.);
#3314=ADVANCED_FACE('',(#402),#3188,.T.);
#3315=ADVANCED_FACE('',(#403),#51,.T.);
#3316=ADVANCED_FACE('',(#404),#52,.T.);
#3317=ADVANCED_FACE('',(#405),#53,.T.);
#3318=ADVANCED_FACE('',(#406),#54,.T.);
#3319=ADVANCED_FACE('',(#407),#284,.T.);
#3320=ADVANCED_FACE('',(#408),#285,.T.);
#3321=ADVANCED_FACE('',(#409),#286,.T.);
#3322=ADVANCED_FACE('',(#410),#287,.T.);
#3323=ADVANCED_FACE('',(#411),#288,.T.);
#3324=ADVANCED_FACE('',(#412),#289,.T.);
#3325=ADVANCED_FACE('',(#413,#221),#290,.T.);
#3326=ADVANCED_FACE('',(#414,#222),#291,.F.);
#3327=ADVANCED_FACE('',(#415),#55,.T.);
#3328=ADVANCED_FACE('',(#416),#56,.T.);
#3329=ADVANCED_FACE('',(#417),#57,.T.);
#3330=ADVANCED_FACE('',(#418),#58,.T.);
#3331=ADVANCED_FACE('',(#419),#59,.T.);
#3332=ADVANCED_FACE('',(#420),#60,.T.);
#3333=ADVANCED_FACE('',(#421),#61,.T.);
#3334=ADVANCED_FACE('',(#422),#62,.T.);
#3335=ADVANCED_FACE('',(#423),#63,.T.);
#3336=ADVANCED_FACE('',(#424),#3189,.T.);
#3337=ADVANCED_FACE('',(#425),#99,.T.);
#3338=ADVANCED_FACE('',(#426),#100,.T.);
#3339=ADVANCED_FACE('',(#427),#101,.T.);
#3340=ADVANCED_FACE('',(#428),#102,.T.);
#3341=ADVANCED_FACE('',(#429),#64,.T.);
#3342=ADVANCED_FACE('',(#430),#65,.T.);
#3343=ADVANCED_FACE('',(#431),#66,.T.);
#3344=ADVANCED_FACE('',(#432),#67,.T.);
#3345=ADVANCED_FACE('',(#433),#103,.T.);
#3346=ADVANCED_FACE('',(#434),#104,.T.);
#3347=ADVANCED_FACE('',(#435),#3190,.T.);
#3348=ADVANCED_FACE('',(#436),#3191,.T.);
#3349=ADVANCED_FACE('',(#437),#105,.T.);
#3350=ADVANCED_FACE('',(#438),#3192,.T.);
#3351=ADVANCED_FACE('',(#439),#106,.T.);
#3352=ADVANCED_FACE('',(#440),#3193,.T.);
#3353=ADVANCED_FACE('',(#441),#68,.T.);
#3354=ADVANCED_FACE('',(#442),#69,.T.);
#3355=ADVANCED_FACE('',(#443),#70,.T.);
#3356=ADVANCED_FACE('',(#444),#71,.T.);
#3357=ADVANCED_FACE('',(#445),#72,.T.);
#3358=ADVANCED_FACE('',(#446),#73,.T.);
#3359=ADVANCED_FACE('',(#447),#3194,.T.);
#3360=ADVANCED_FACE('',(#448),#107,.T.);
#3361=ADVANCED_FACE('',(#449),#108,.T.);
#3362=ADVANCED_FACE('',(#450),#109,.T.);
#3363=ADVANCED_FACE('',(#451),#110,.T.);
#3364=ADVANCED_FACE('',(#452),#111,.T.);
#3365=ADVANCED_FACE('',(#453),#112,.T.);
#3366=ADVANCED_FACE('',(#454),#113,.T.);
#3367=ADVANCED_FACE('',(#455),#74,.T.);
#3368=ADVANCED_FACE('',(#456),#75,.T.);
#3369=ADVANCED_FACE('',(#457),#76,.T.);
#3370=ADVANCED_FACE('',(#458),#77,.T.);
#3371=ADVANCED_FACE('',(#459),#78,.T.);
#3372=ADVANCED_FACE('',(#460),#79,.T.);
#3373=ADVANCED_FACE('',(#461),#114,.T.);
#3374=ADVANCED_FACE('',(#462),#115,.T.);
#3375=ADVANCED_FACE('',(#463),#116,.T.);
#3376=ADVANCED_FACE('',(#464),#3195,.T.);
#3377=ADVANCED_FACE('',(#465),#3196,.T.);
#3378=ADVANCED_FACE('',(#466),#117,.T.);
#3379=ADVANCED_FACE('',(#467),#3197,.T.);
#3380=ADVANCED_FACE('',(#468),#3198,.T.);
#3381=ADVANCED_FACE('',(#469),#118,.T.);
#3382=ADVANCED_FACE('',(#470),#80,.T.);
#3383=ADVANCED_FACE('',(#471),#81,.T.);
#3384=ADVANCED_FACE('',(#472),#82,.T.);
#3385=ADVANCED_FACE('',(#473),#83,.T.);
#3386=ADVANCED_FACE('',(#474),#84,.T.);
#3387=ADVANCED_FACE('',(#475),#85,.T.);
#3388=ADVANCED_FACE('',(#476),#86,.T.);
#3389=ADVANCED_FACE('',(#477),#3199,.T.);
#3390=ADVANCED_FACE('',(#478),#3200,.T.);
#3391=ADVANCED_FACE('',(#479),#119,.T.);
#3392=ADVANCED_FACE('',(#480),#120,.T.);
#3393=ADVANCED_FACE('',(#481),#121,.T.);
#3394=ADVANCED_FACE('',(#482),#122,.T.);
#3395=ADVANCED_FACE('',(#483),#123,.T.);
#3396=ADVANCED_FACE('',(#484),#124,.T.);
#3397=ADVANCED_FACE('',(#485),#125,.T.);
#3398=ADVANCED_FACE('',(#486),#87,.T.);
#3399=ADVANCED_FACE('',(#487),#88,.T.);
#3400=ADVANCED_FACE('',(#488),#89,.T.);
#3401=ADVANCED_FACE('',(#489),#90,.T.);
#3402=ADVANCED_FACE('',(#490),#3201,.T.);
#3403=ADVANCED_FACE('',(#491),#126,.T.);
#3404=ADVANCED_FACE('',(#492),#3202,.T.);
#3405=ADVANCED_FACE('',(#493),#3203,.T.);
#3406=ADVANCED_FACE('',(#494),#127,.T.);
#3407=ADVANCED_FACE('',(#495),#3204,.T.);
#3408=ADVANCED_FACE('',(#496),#91,.T.);
#3409=ADVANCED_FACE('',(#497),#92,.T.);
#3410=ADVANCED_FACE('',(#498),#93,.T.);
#3411=ADVANCED_FACE('',(#499),#94,.T.);
#3412=ADVANCED_FACE('',(#500),#128,.T.);
#3413=ADVANCED_FACE('',(#501),#129,.T.);
#3414=ADVANCED_FACE('',(#502),#130,.T.);
#3415=ADVANCED_FACE('',(#503),#131,.T.);
#3416=ADVANCED_FACE('',(#504),#95,.T.);
#3417=ADVANCED_FACE('',(#505),#96,.T.);
#3418=ADVANCED_FACE('',(#506),#3205,.T.);
#3419=ADVANCED_FACE('',(#507),#292,.T.);
#3432=CLOSED_SHELL('',(#3308,#3309,#3310,#3311,#3312,#3313,#3314,#3315,
#3316,#3317,#3318,#3319,#3320,#3321,#3322,#3323,#3324,#3325,#3326,#3327,
#3328,#3329,#3330,#3331,#3332,#3333,#3334,#3335,#3336,#3337,#3338,#3339,
#3340,#3341,#3342,#3343,#3344,#3345,#3346,#3347,#3348,#3349,#3350,#3351,
#3352,#3353,#3354,#3355,#3356,#3357,#3358,#3359,#3360,#3361,#3362,#3363,
#3364,#3365,#3366,#3367,#3368,#3369,#3370,#3371,#3372,#3373,#3374,#3375,
#3376,#3377,#3378,#3379,#3380,#3381,#3382,#3383,#3384,#3385,#3386,#3387,
#3388,#3389,#3390,#3391,#3392,#3393,#3394,#3395,#3396,#3397,#3398,#3399,
#3400,#3401,#3402,#3403,#3404,#3405,#3406,#3407,#3408,#3409,#3410,#3411,
#3412,#3413,#3414,#3415,#3416,#3417,#3418,#3419));
#3718=AXIS2_PLACEMENT_3D('',#7892,#4558,#4559);
#3719=AXIS2_PLACEMENT_3D('',#7893,#4560,#4561);
#3720=AXIS2_PLACEMENT_3D('',#7895,#4562,#4563);
#3721=AXIS2_PLACEMENT_3D('',#7898,#4565,#4566);
#3722=AXIS2_PLACEMENT_3D('',#7899,#4567,#4568);
#3723=AXIS2_PLACEMENT_3D('',#7901,#4569,#4570);
#3724=AXIS2_PLACEMENT_3D('',#7903,#4572,#4573);
#3725=AXIS2_PLACEMENT_3D('',#7906,#4574,#4575);
#3726=AXIS2_PLACEMENT_3D('',#7908,#4576,#4577);
#3727=AXIS2_PLACEMENT_3D('',#7910,#4578,#4579);
#3728=AXIS2_PLACEMENT_3D('',#7911,#4580,#4581);
#3729=AXIS2_PLACEMENT_3D('',#7912,#4582,#4583);
#3730=AXIS2_PLACEMENT_3D('',#7915,#4584,#4585);
#3731=AXIS2_PLACEMENT_3D('',#7919,#4587,#4588);
#3732=AXIS2_PLACEMENT_3D('',#7921,#4590,#4591);
#3733=AXIS2_PLACEMENT_3D('',#7924,#4592,#4593);
#3734=AXIS2_PLACEMENT_3D('',#7926,#4594,#4595);
#3735=AXIS2_PLACEMENT_3D('',#7928,#4596,#4597);
#3736=AXIS2_PLACEMENT_3D('',#7929,#4598,#4599);
#3737=AXIS2_PLACEMENT_3D('',#7930,#4600,#4601);
#3738=AXIS2_PLACEMENT_3D('',#7932,#4602,#4603);
#3739=AXIS2_PLACEMENT_3D('',#7934,#4604,#4605);
#3740=AXIS2_PLACEMENT_3D('',#7935,#4606,#4607);
#3741=AXIS2_PLACEMENT_3D('',#7937,#4608,#4609);
#3742=AXIS2_PLACEMENT_3D('',#7939,#4611,#4612);
#3743=AXIS2_PLACEMENT_3D('',#7942,#4613,#4614);
#3744=AXIS2_PLACEMENT_3D('',#7944,#4615,#4616);
#3745=AXIS2_PLACEMENT_3D('',#7945,#4617,#4618);
#3746=AXIS2_PLACEMENT_3D('',#7946,#4619,#4620);
#3747=AXIS2_PLACEMENT_3D('',#7949,#4621,#4622);
#3748=AXIS2_PLACEMENT_3D('',#7951,#4623,#4624);
#3749=AXIS2_PLACEMENT_3D('',#7952,#4625,#4626);
#3750=AXIS2_PLACEMENT_3D('',#7953,#4627,#4628);
#3751=AXIS2_PLACEMENT_3D('',#7956,#4629,#4630);
#3752=AXIS2_PLACEMENT_3D('',#7958,#4631,#4632);
#3753=AXIS2_PLACEMENT_3D('',#7959,#4633,#4634);
#3754=AXIS2_PLACEMENT_3D('',#7960,#4635,#4636);
#3755=AXIS2_PLACEMENT_3D('',#7963,#4637,#4638);
#3756=AXIS2_PLACEMENT_3D('',#7965,#4639,#4640);
#3757=AXIS2_PLACEMENT_3D('',#7966,#4641,#4642);
#3758=AXIS2_PLACEMENT_3D('',#7967,#4643,#4644);
#3759=AXIS2_PLACEMENT_3D('',#7972,#4646,#4647);
#3760=AXIS2_PLACEMENT_3D('',#7976,#4649,#4650);
#3761=AXIS2_PLACEMENT_3D('',#7980,#4652,#4653);
#3762=AXIS2_PLACEMENT_3D('',#7983,#4655,#4656);
#3763=AXIS2_PLACEMENT_3D('',#7984,#4657,#4658);
#3764=AXIS2_PLACEMENT_3D('',#7987,#4659,#4660);
#3765=AXIS2_PLACEMENT_3D('',#7991,#4662,#4663);
#3766=AXIS2_PLACEMENT_3D('',#7995,#4665,#4666);
#3767=AXIS2_PLACEMENT_3D('',#7999,#4668,#4669);
#3768=AXIS2_PLACEMENT_3D('',#8001,#4671,#4672);
#3769=AXIS2_PLACEMENT_3D('',#8004,#4673,#4674);
#3770=AXIS2_PLACEMENT_3D('',#8008,#4676,#4677);
#3771=AXIS2_PLACEMENT_3D('',#8012,#4679,#4680);
#3772=AXIS2_PLACEMENT_3D('',#8016,#4682,#4683);
#3773=AXIS2_PLACEMENT_3D('',#8018,#4685,#4686);
#3774=AXIS2_PLACEMENT_3D('',#8021,#4687,#4688);
#3775=AXIS2_PLACEMENT_3D('',#8025,#4690,#4691);
#3776=AXIS2_PLACEMENT_3D('',#8029,#4693,#4694);
#3777=AXIS2_PLACEMENT_3D('',#8033,#4696,#4697);
#3778=AXIS2_PLACEMENT_3D('',#8035,#4699,#4700);
#3779=AXIS2_PLACEMENT_3D('',#8037,#4701,#4702);
#3780=AXIS2_PLACEMENT_3D('',#8041,#4704,#4705);
#3781=AXIS2_PLACEMENT_3D('',#8045,#4707,#4708);
#3782=AXIS2_PLACEMENT_3D('',#8048,#4710,#4711);
#3783=AXIS2_PLACEMENT_3D('',#8049,#4712,#4713);
#3784=AXIS2_PLACEMENT_3D('',#8052,#4714,#4715);
#3785=AXIS2_PLACEMENT_3D('',#8055,#4717,#4718);
#3786=AXIS2_PLACEMENT_3D('',#8057,#4719,#4720);
#3787=AXIS2_PLACEMENT_3D('',#8061,#4722,#4723);
#3788=AXIS2_PLACEMENT_3D('',#8063,#4725,#4726);
#3789=AXIS2_PLACEMENT_3D('',#8066,#4727,#4728);
#3790=AXIS2_PLACEMENT_3D('',#8070,#4730,#4731);
#3791=AXIS2_PLACEMENT_3D('',#8075,#4734,#4735);
#3792=AXIS2_PLACEMENT_3D('',#8079,#4737,#4738);
#3793=AXIS2_PLACEMENT_3D('',#8083,#4740,#4741);
#3794=AXIS2_PLACEMENT_3D('',#8085,#4743,#4744);
#3795=AXIS2_PLACEMENT_3D('',#8090,#4746,#4747);
#3796=AXIS2_PLACEMENT_3D('',#8095,#4750,#4751);
#3797=AXIS2_PLACEMENT_3D('',#8099,#4753,#4754);
#3798=AXIS2_PLACEMENT_3D('',#8103,#4756,#4757);
#3799=AXIS2_PLACEMENT_3D('',#8106,#4759,#4760);
#3800=AXIS2_PLACEMENT_3D('',#8107,#4761,#4762);
#3801=AXIS2_PLACEMENT_3D('',#8109,#4763,#4764);
#3802=AXIS2_PLACEMENT_3D('',#8110,#4765,#4766);
#3803=AXIS2_PLACEMENT_3D('',#8111,#4767,#4768);
#3804=AXIS2_PLACEMENT_3D('',#8114,#4769,#4770);
#3805=AXIS2_PLACEMENT_3D('',#8116,#4771,#4772);
#3806=AXIS2_PLACEMENT_3D('',#8117,#4773,#4774);
#3807=AXIS2_PLACEMENT_3D('',#8118,#4775,#4776);
#3808=AXIS2_PLACEMENT_3D('',#8121,#4777,#4778);
#3809=AXIS2_PLACEMENT_3D('',#8123,#4779,#4780);
#3810=AXIS2_PLACEMENT_3D('',#8124,#4781,#4782);
#3811=AXIS2_PLACEMENT_3D('',#8125,#4783,#4784);
#3812=AXIS2_PLACEMENT_3D('',#8128,#4785,#4786);
#3813=AXIS2_PLACEMENT_3D('',#8154,#4787,#4788);
#3814=AXIS2_PLACEMENT_3D('',#8155,#4789,#4790);
#3815=AXIS2_PLACEMENT_3D('',#8157,#4791,#4792);
#3816=AXIS2_PLACEMENT_3D('',#8158,#4793,#4794);
#3817=AXIS2_PLACEMENT_3D('',#8159,#4795,#4796);
#3818=AXIS2_PLACEMENT_3D('',#8162,#4797,#4798);
#3819=AXIS2_PLACEMENT_3D('',#8164,#4799,#4800);
#3820=AXIS2_PLACEMENT_3D('',#8165,#4801,#4802);
#3821=AXIS2_PLACEMENT_3D('',#8166,#4803,#4804);
#3822=AXIS2_PLACEMENT_3D('',#8169,#4805,#4806);
#3823=AXIS2_PLACEMENT_3D('',#8171,#4807,#4808);
#3824=AXIS2_PLACEMENT_3D('',#8172,#4809,#4810);
#3825=AXIS2_PLACEMENT_3D('',#8173,#4811,#4812);
#3826=AXIS2_PLACEMENT_3D('',#8176,#4813,#4814);
#3827=AXIS2_PLACEMENT_3D('',#8178,#4815,#4816);
#3828=AXIS2_PLACEMENT_3D('',#8179,#4817,#4818);
#3829=AXIS2_PLACEMENT_3D('',#8180,#4819,#4820);
#3830=AXIS2_PLACEMENT_3D('',#8181,#4821,#4822);
#3831=AXIS2_PLACEMENT_3D('',#8182,#4823,#4824);
#3832=AXIS2_PLACEMENT_3D('',#8183,#4825,#4826);
#3833=AXIS2_PLACEMENT_3D('',#8184,#4827,#4828);
#3834=AXIS2_PLACEMENT_3D('',#8185,#4829,#4830);
#3835=AXIS2_PLACEMENT_3D('',#8186,#4831,#4832);
#3836=AXIS2_PLACEMENT_3D('',#8187,#4833,#4834);
#3837=AXIS2_PLACEMENT_3D('',#8188,#4835,#4836);
#3838=AXIS2_PLACEMENT_3D('',#8189,#4837,#4838);
#3839=AXIS2_PLACEMENT_3D('',#8190,#4839,#4840);
#3840=AXIS2_PLACEMENT_3D('',#8191,#4841,#4842);
#3841=AXIS2_PLACEMENT_3D('',#8192,#4843,#4844);
#3842=AXIS2_PLACEMENT_3D('',#8193,#4845,#4846);
#3843=AXIS2_PLACEMENT_3D('',#8194,#4847,#4848);
#3844=AXIS2_PLACEMENT_3D('',#8195,#4849,#4850);
#3845=AXIS2_PLACEMENT_3D('',#8196,#4851,#4852);
#3846=AXIS2_PLACEMENT_3D('',#8197,#4853,#4854);
#3847=AXIS2_PLACEMENT_3D('',#8198,#4855,#4856);
#3848=AXIS2_PLACEMENT_3D('',#8199,#4857,#4858);
#3849=AXIS2_PLACEMENT_3D('',#8200,#4859,#4860);
#3850=AXIS2_PLACEMENT_3D('',#8201,#4861,#4862);
#3851=AXIS2_PLACEMENT_3D('',#8202,#4863,#4864);
#3852=AXIS2_PLACEMENT_3D('',#8203,#4865,#4866);
#3853=AXIS2_PLACEMENT_3D('',#8204,#4867,#4868);
#3854=AXIS2_PLACEMENT_3D('',#8205,#4869,#4870);
#3855=AXIS2_PLACEMENT_3D('',#8206,#4871,#4872);
#3856=AXIS2_PLACEMENT_3D('',#8207,#4873,#4874);
#3857=AXIS2_PLACEMENT_3D('',#8208,#4875,#4876);
#3858=AXIS2_PLACEMENT_3D('',#8209,#4877,#4878);
#3859=AXIS2_PLACEMENT_3D('',#8210,#4879,#4880);
#3860=AXIS2_PLACEMENT_3D('',#8211,#4881,#4882);
#3861=AXIS2_PLACEMENT_3D('',#8212,#4883,#4884);
#3862=AXIS2_PLACEMENT_3D('',#8213,#4885,#4886);
#3863=AXIS2_PLACEMENT_3D('',#8214,#4887,#4888);
#3864=AXIS2_PLACEMENT_3D('',#8215,#4889,#4890);
#3865=AXIS2_PLACEMENT_3D('',#8216,#4891,#4892);
#3866=AXIS2_PLACEMENT_3D('',#8217,#4893,#4894);
#3867=AXIS2_PLACEMENT_3D('',#8218,#4895,#4896);
#3868=AXIS2_PLACEMENT_3D('',#8219,#4897,#4898);
#3869=AXIS2_PLACEMENT_3D('',#8220,#4899,#4900);
#3870=AXIS2_PLACEMENT_3D('',#8221,#4901,#4902);
#3871=AXIS2_PLACEMENT_3D('',#8222,#4903,#4904);
#3872=AXIS2_PLACEMENT_3D('',#8223,#4905,#4906);
#3873=AXIS2_PLACEMENT_3D('',#8224,#4907,#4908);
#3874=AXIS2_PLACEMENT_3D('',#8225,#4909,#4910);
#3875=AXIS2_PLACEMENT_3D('',#8226,#4911,#4912);
#3876=AXIS2_PLACEMENT_3D('',#8227,#4913,#4914);
#3877=AXIS2_PLACEMENT_3D('',#8228,#4915,#4916);
#3878=AXIS2_PLACEMENT_3D('',#8229,#4917,#4918);
#3879=AXIS2_PLACEMENT_3D('',#8230,#4919,#4920);
#3880=AXIS2_PLACEMENT_3D('',#8231,#4921,#4922);
#3881=AXIS2_PLACEMENT_3D('',#8232,#4923,#4924);
#3882=AXIS2_PLACEMENT_3D('',#8233,#4925,#4926);
#3883=AXIS2_PLACEMENT_3D('',#8234,#4927,#4928);
#3884=AXIS2_PLACEMENT_3D('',#8235,#4929,#4930);
#3885=AXIS2_PLACEMENT_3D('',#8236,#4931,#4932);
#3886=AXIS2_PLACEMENT_3D('',#8237,#4933,#4934);
#3887=AXIS2_PLACEMENT_3D('',#8238,#4935,#4936);
#3888=AXIS2_PLACEMENT_3D('',#8239,#4937,#4938);
#3889=AXIS2_PLACEMENT_3D('',#8240,#4939,#4940);
#3890=AXIS2_PLACEMENT_3D('',#8241,#4941,#4942);
#3891=AXIS2_PLACEMENT_3D('',#8242,#4943,#4944);
#3892=AXIS2_PLACEMENT_3D('',#8243,#4945,#4946);
#3893=AXIS2_PLACEMENT_3D('',#8244,#4947,#4948);
#3894=AXIS2_PLACEMENT_3D('',#8245,#4949,#4950);
#3895=AXIS2_PLACEMENT_3D('',#8246,#4951,#4952);
#3896=AXIS2_PLACEMENT_3D('',#8247,#4953,#4954);
#3897=AXIS2_PLACEMENT_3D('',#8248,#4955,#4956);
#3898=AXIS2_PLACEMENT_3D('',#8249,#4957,#4958);
#3899=AXIS2_PLACEMENT_3D('',#8250,#4959,#4960);
#3900=AXIS2_PLACEMENT_3D('',#8251,#4961,#4962);
#3901=AXIS2_PLACEMENT_3D('',#8252,#4963,#4964);
#3902=AXIS2_PLACEMENT_3D('',#8253,#4965,#4966);
#3903=AXIS2_PLACEMENT_3D('',#8254,#4967,#4968);
#3904=AXIS2_PLACEMENT_3D('',#8255,#4969,#4970);
#3905=AXIS2_PLACEMENT_3D('',#8256,#4971,#4972);
#3906=AXIS2_PLACEMENT_3D('',#8257,#4973,#4974);
#3907=AXIS2_PLACEMENT_3D('',#8258,#4975,#4976);
#3908=AXIS2_PLACEMENT_3D('',#8259,#4977,#4978);
#3909=AXIS2_PLACEMENT_3D('',#8260,#4979,#4980);
#3910=AXIS2_PLACEMENT_3D('',#8261,#4981,#4982);
#3911=AXIS2_PLACEMENT_3D('',#8262,#4983,#4984);
#3912=AXIS2_PLACEMENT_3D('',#8263,#4985,#4986);
#3913=AXIS2_PLACEMENT_3D('',#8264,#4987,#4988);
#3914=AXIS2_PLACEMENT_3D('',#8265,#4989,#4990);
#3915=AXIS2_PLACEMENT_3D('',#8266,#4991,#4992);
#3916=AXIS2_PLACEMENT_3D('',#8267,#4993,#4994);
#3917=AXIS2_PLACEMENT_3D('',#8268,#4995,#4996);
#3918=AXIS2_PLACEMENT_3D('',#8269,#4997,#4998);
#3919=AXIS2_PLACEMENT_3D('',#8270,#4999,#5000);
#3920=AXIS2_PLACEMENT_3D('',#8271,#5001,#5002);
#3921=AXIS2_PLACEMENT_3D('',#8272,#5003,#5004);
#3922=AXIS2_PLACEMENT_3D('',#8273,#5005,#5006);
#3923=AXIS2_PLACEMENT_3D('',#8274,#5007,#5008);
#3924=AXIS2_PLACEMENT_3D('',#8275,#5009,#5010);
#3925=AXIS2_PLACEMENT_3D('',#8276,#5011,#5012);
#3926=AXIS2_PLACEMENT_3D('',#8277,#5013,#5014);
#3927=AXIS2_PLACEMENT_3D('',#8278,#5015,#5016);
#3928=AXIS2_PLACEMENT_3D('',#8279,#5017,#5018);
#3929=AXIS2_PLACEMENT_3D('',#8280,#5019,#5020);
#3930=AXIS2_PLACEMENT_3D('',#8281,#5021,#5022);
#3931=AXIS2_PLACEMENT_3D('',#8282,#5023,#5024);
#3932=AXIS2_PLACEMENT_3D('',#8283,#5025,#5026);
#3933=AXIS2_PLACEMENT_3D('',#8284,#5027,#5028);
#3934=AXIS2_PLACEMENT_3D('',#8285,#5029,#5030);
#3935=AXIS2_PLACEMENT_3D('',#8286,#5031,#5032);
#3936=AXIS2_PLACEMENT_3D('',#8287,#5033,#5034);
#3937=AXIS2_PLACEMENT_3D('',#8288,#5035,#5036);
#3938=AXIS2_PLACEMENT_3D('',#8289,#5037,#5038);
#3939=AXIS2_PLACEMENT_3D('',#8290,#5039,#5040);
#3940=AXIS2_PLACEMENT_3D('',#8291,#5041,#5042);
#3941=AXIS2_PLACEMENT_3D('',#8292,#5043,#5044);
#3942=AXIS2_PLACEMENT_3D('',#8293,#5045,#5046);
#3943=AXIS2_PLACEMENT_3D('',#8294,#5047,#5048);
#3944=AXIS2_PLACEMENT_3D('',#8295,#5049,#5050);
#3945=AXIS2_PLACEMENT_3D('',#8296,#5051,#5052);
#3946=AXIS2_PLACEMENT_3D('',#8297,#5053,#5054);
#3947=AXIS2_PLACEMENT_3D('',#8298,#5055,#5056);
#3948=AXIS2_PLACEMENT_3D('',#8299,#5057,#5058);
#3949=AXIS2_PLACEMENT_3D('',#8300,#5059,#5060);
#3950=AXIS2_PLACEMENT_3D('',#8301,#5061,#5062);
#3951=AXIS2_PLACEMENT_3D('',#8302,#5063,#5064);
#3952=AXIS2_PLACEMENT_3D('',#8303,#5065,#5066);
#3953=AXIS2_PLACEMENT_3D('',#8304,#5067,#5068);
#3954=AXIS2_PLACEMENT_3D('',#8305,#5069,#5070);
#3955=AXIS2_PLACEMENT_3D('',#8306,#5071,#5072);
#3956=AXIS2_PLACEMENT_3D('',#8307,#5073,#5074);
#3957=AXIS2_PLACEMENT_3D('',#8308,#5075,#5076);
#3958=AXIS2_PLACEMENT_3D('',#8309,#5077,#5078);
#3959=AXIS2_PLACEMENT_3D('',#8310,#5079,#5080);
#3960=AXIS2_PLACEMENT_3D('',#8311,#5081,#5082);
#3961=AXIS2_PLACEMENT_3D('',#8312,#5083,#5084);
#3962=AXIS2_PLACEMENT_3D('',#8313,#5085,#5086);
#3963=AXIS2_PLACEMENT_3D('',#8314,#5087,#5088);
#3964=AXIS2_PLACEMENT_3D('',#8315,#5089,#5090);
#3965=AXIS2_PLACEMENT_3D('',#8316,#5091,#5092);
#3966=AXIS2_PLACEMENT_3D('',#8317,#5093,#5094);
#3967=AXIS2_PLACEMENT_3D('',#8318,#5095,#5096);
#3968=AXIS2_PLACEMENT_3D('',#8319,#5097,#5098);
#3969=AXIS2_PLACEMENT_3D('',#8320,#5099,#5100);
#3970=AXIS2_PLACEMENT_3D('',#8321,#5101,#5102);
#3971=AXIS2_PLACEMENT_3D('',#8322,#5103,#5104);
#3972=AXIS2_PLACEMENT_3D('',#8323,#5105,#5106);
#3973=AXIS2_PLACEMENT_3D('',#8324,#5107,#5108);
#3974=AXIS2_PLACEMENT_3D('',#8325,#5109,#5110);
#3975=AXIS2_PLACEMENT_3D('',#8326,#5111,#5112);
#3976=AXIS2_PLACEMENT_3D('',#8327,#5113,#5114);
#3977=AXIS2_PLACEMENT_3D('',#8328,#5115,#5116);
#3978=AXIS2_PLACEMENT_3D('',#8329,#5117,#5118);
#3979=AXIS2_PLACEMENT_3D('',#8330,#5119,#5120);
#3980=AXIS2_PLACEMENT_3D('',#8331,#5121,#5122);
#3981=AXIS2_PLACEMENT_3D('',#8332,#5123,#5124);
#3982=AXIS2_PLACEMENT_3D('',#8333,#5125,#5126);
#3983=AXIS2_PLACEMENT_3D('',#8334,#5127,#5128);
#3984=AXIS2_PLACEMENT_3D('',#8335,#5129,#5130);
#3985=AXIS2_PLACEMENT_3D('',#8336,#5131,#5132);
#3986=AXIS2_PLACEMENT_3D('',#8337,#5133,#5134);
#3987=AXIS2_PLACEMENT_3D('',#8338,#5135,#5136);
#3988=AXIS2_PLACEMENT_3D('',#8339,#5137,#5138);
#3989=AXIS2_PLACEMENT_3D('',#8340,#5139,#5140);
#3990=AXIS2_PLACEMENT_3D('',#8341,#5141,#5142);
#3991=AXIS2_PLACEMENT_3D('',#8342,#5143,#5144);
#3992=AXIS2_PLACEMENT_3D('',#8343,#5145,#5146);
#3993=AXIS2_PLACEMENT_3D('',#8344,#5147,#5148);
#3994=AXIS2_PLACEMENT_3D('',#8345,#5149,#5150);
#3995=AXIS2_PLACEMENT_3D('',#8346,#5151,#5152);
#3996=AXIS2_PLACEMENT_3D('',#8347,#5153,#5154);
#3997=AXIS2_PLACEMENT_3D('',#8348,#5155,#5156);
#3998=AXIS2_PLACEMENT_3D('',#8349,#5157,#5158);
#3999=AXIS2_PLACEMENT_3D('',#8350,#5159,#5160);
#4000=AXIS2_PLACEMENT_3D('',#8351,#5161,#5162);
#4001=AXIS2_PLACEMENT_3D('',#8352,#5163,#5164);
#4002=AXIS2_PLACEMENT_3D('',#8353,#5165,#5166);
#4003=AXIS2_PLACEMENT_3D('',#8354,#5167,#5168);
#4004=AXIS2_PLACEMENT_3D('',#8355,#5169,#5170);
#4005=AXIS2_PLACEMENT_3D('',#8356,#5171,#5172);
#4006=AXIS2_PLACEMENT_3D('',#8357,#5173,#5174);
#4007=AXIS2_PLACEMENT_3D('',#8358,#5175,#5176);
#4008=AXIS2_PLACEMENT_3D('',#8359,#5177,#5178);
#4009=AXIS2_PLACEMENT_3D('',#8360,#5179,#5180);
#4010=AXIS2_PLACEMENT_3D('',#8361,#5181,#5182);
#4011=AXIS2_PLACEMENT_3D('',#8362,#5183,#5184);
#4558=DIRECTION('axis',(0.,0.,1.));
#4559=DIRECTION('refdir',(1.,0.,0.));
#4560=DIRECTION('center_axis',(0.,-1.,0.));
#4561=DIRECTION('ref_axis',(0.,0.,-1.));
#4562=DIRECTION('center_axis',(0.,-1.,0.));
#4563=DIRECTION('ref_axis',(0.,0.,1.));
#4564=DIRECTION('',(-8.65956056235497E-17,-0.707106781186544,0.707106781186551));
#4565=DIRECTION('center_axis',(0.,1.,0.));
#4566=DIRECTION('ref_axis',(0.,0.,1.));
#4567=DIRECTION('center_axis',(0.,-1.,0.));
#4568=DIRECTION('ref_axis',(0.,0.,-1.));
#4569=DIRECTION('center_axis',(0.,-1.,0.));
#4570=DIRECTION('ref_axis',(0.,0.,-1.));
#4571=DIRECTION('',(0.,-1.,0.));
#4572=DIRECTION('center_axis',(0.,1.,0.));
#4573=DIRECTION('ref_axis',(0.,0.,1.));
#4574=DIRECTION('center_axis',(0.,-1.,0.));
#4575=DIRECTION('ref_axis',(0.,0.,1.));
#4576=DIRECTION('center_axis',(-0.948250947674427,-6.78917425016181E-14,
0.317521873631646));
#4577=DIRECTION('ref_axis',(-0.317521873631646,-4.81926486971319E-29,-0.948250947674427));
#4578=DIRECTION('center_axis',(0.,1.,0.));
#4579=DIRECTION('ref_axis',(0.,0.,1.));
#4580=DIRECTION('center_axis',(-0.94825094767444,0.,-0.317521873631608));
#4581=DIRECTION('ref_axis',(-0.317521873631608,0.,0.94825094767444));
#4582=DIRECTION('center_axis',(0.,-1.,0.));
#4583=DIRECTION('ref_axis',(0.,0.,-1.));
#4584=DIRECTION('center_axis',(8.67361737988396E-15,-1.,5.0077153291238E-15));
#4585=DIRECTION('ref_axis',(-1.,-8.673617379884E-15,-8.67361737988403E-15));
#4586=DIRECTION('',(0.,1.,0.));
#4587=DIRECTION('center_axis',(-3.25260651745648E-15,-1.,1.87789324842143E-15));
#4588=DIRECTION('ref_axis',(1.,-3.25260651745648E-15,-5.46506401086679E-44));
#4589=DIRECTION('',(0.,-1.,0.));
#4590=DIRECTION('center_axis',(0.,1.,0.));
#4591=DIRECTION('ref_axis',(0.,0.,1.));
#4592=DIRECTION('center_axis',(0.,-1.,0.));
#4593=DIRECTION('ref_axis',(0.,0.,-1.));
#4594=DIRECTION('center_axis',(-0.948250947674425,0.,0.317521873631651));
#4595=DIRECTION('ref_axis',(-0.317521873631651,4.33680868994201E-14,-0.948250947674425));
#4596=DIRECTION('center_axis',(0.,1.,0.));
#4597=DIRECTION('ref_axis',(0.,0.,1.));
#4598=DIRECTION('center_axis',(-0.948250947674424,-6.03274245433074E-14,
-0.317521873631656));
#4599=DIRECTION('ref_axis',(-0.317521873631656,1.27015359233011E-28,0.948250947674424));
#4600=DIRECTION('center_axis',(0.,1.,-6.12323399573676E-17));
#4601=DIRECTION('ref_axis',(0.,0.,-1.));
#4602=DIRECTION('center_axis',(0.,-1.,0.));
#4603=DIRECTION('ref_axis',(0.,0.,-1.));
#4604=DIRECTION('center_axis',(1.,0.,-1.22464679914735E-16));
#4605=DIRECTION('ref_axis',(1.22464679914735E-16,0.,1.));
#4606=DIRECTION('center_axis',(0.,-1.,0.));
#4607=DIRECTION('ref_axis',(0.,0.,-1.));
#4608=DIRECTION('center_axis',(0.,1.,0.));
#4609=DIRECTION('ref_axis',(0.,0.,1.));
#4610=DIRECTION('',(0.,1.,0.));
#4611=DIRECTION('center_axis',(-0.5,0.,-0.866025403784439));
#4612=DIRECTION('ref_axis',(0.866025403784439,0.,-0.5));
#4613=DIRECTION('center_axis',(0.,1.,0.));
#4614=DIRECTION('ref_axis',(0.,0.,1.));
#4615=DIRECTION('center_axis',(0.5,0.,-0.866025403784439));
#4616=DIRECTION('ref_axis',(-0.866025403784439,0.,-0.5));
#4617=DIRECTION('center_axis',(1.,0.,0.));
#4618=DIRECTION('ref_axis',(0.,0.,-1.));
#4619=DIRECTION('center_axis',(-0.5,0.,-0.866025403784439));
#4620=DIRECTION('ref_axis',(0.866025403784439,0.,-0.5));
#4621=DIRECTION('center_axis',(0.,1.,0.));
#4622=DIRECTION('ref_axis',(0.,0.,1.));
#4623=DIRECTION('center_axis',(-0.5,0.,0.866025403784439));
#4624=DIRECTION('ref_axis',(0.866025403784439,0.,0.5));
#4625=DIRECTION('center_axis',(-1.,0.,0.));
#4626=DIRECTION('ref_axis',(0.,0.,1.));
#4627=DIRECTION('center_axis',(0.5,0.,0.866025403784438));
#4628=DIRECTION('ref_axis',(0.866025403784439,0.,-0.5));
#4629=DIRECTION('center_axis',(0.,-1.,0.));
#4630=DIRECTION('ref_axis',(0.,0.,-1.));
#4631=DIRECTION('center_axis',(1.,0.,0.));
#4632=DIRECTION('ref_axis',(0.,0.,-1.));
#4633=DIRECTION('center_axis',(0.5,0.,-0.866025403784439));
#4634=DIRECTION('ref_axis',(-0.866025403784439,0.,-0.5));
#4635=DIRECTION('center_axis',(0.5,0.,0.866025403784438));
#4636=DIRECTION('ref_axis',(0.866025403784439,0.,-0.5));
#4637=DIRECTION('center_axis',(0.,-1.,0.));
#4638=DIRECTION('ref_axis',(0.,0.,-1.));
#4639=DIRECTION('center_axis',(-1.,0.,0.));
#4640=DIRECTION('ref_axis',(0.,0.,1.));
#4641=DIRECTION('center_axis',(-0.5,0.,0.866025403784439));
#4642=DIRECTION('ref_axis',(0.866025403784439,0.,0.5));
#4643=DIRECTION('center_axis',(-1.,0.,0.));
#4644=DIRECTION('ref_axis',(0.,0.,1.));
#4645=DIRECTION('',(0.,-1.,0.));
#4646=DIRECTION('center_axis',(-1.,0.,0.));
#4647=DIRECTION('ref_axis',(0.,0.,1.));
#4648=DIRECTION('',(0.,0.,1.));
#4649=DIRECTION('center_axis',(-1.,0.,0.));
#4650=DIRECTION('ref_axis',(0.,0.,1.));
#4651=DIRECTION('',(0.,1.,0.));
#4652=DIRECTION('center_axis',(-1.,0.,0.));
#4653=DIRECTION('ref_axis',(0.,0.,1.));
#4654=DIRECTION('',(0.,0.,-1.));
#4655=DIRECTION('center_axis',(-1.,0.,0.));
#4656=DIRECTION('ref_axis',(0.,0.,1.));
#4657=DIRECTION('center_axis',(-0.5,0.,0.866025403784439));
#4658=DIRECTION('ref_axis',(0.866025403784439,0.,0.5));
#4659=DIRECTION('center_axis',(-0.5,0.,0.866025403784439));
#4660=DIRECTION('ref_axis',(0.866025403784439,0.,0.5));
#4661=DIRECTION('',(0.866025403784439,0.,0.5));
#4662=DIRECTION('center_axis',(-0.5,0.,0.866025403784439));
#4663=DIRECTION('ref_axis',(0.866025403784439,0.,0.5));
#4664=DIRECTION('',(0.,1.,0.));
#4665=DIRECTION('center_axis',(-0.5,0.,0.866025403784439));
#4666=DIRECTION('ref_axis',(0.866025403784439,0.,0.5));
#4667=DIRECTION('',(-0.866025403784439,0.,-0.5));
#4668=DIRECTION('center_axis',(-0.5,0.,0.866025403784439));
#4669=DIRECTION('ref_axis',(0.866025403784439,0.,0.5));
#4670=DIRECTION('',(0.,-1.,0.));
#4671=DIRECTION('center_axis',(0.5,0.,0.866025403784439));
#4672=DIRECTION('ref_axis',(0.866025403784439,0.,-0.5));
#4673=DIRECTION('center_axis',(0.5,0.,0.866025403784439));
#4674=DIRECTION('ref_axis',(0.866025403784439,0.,-0.5));
#4675=DIRECTION('',(0.866025403784439,0.,-0.5));
#4676=DIRECTION('center_axis',(0.5,0.,0.866025403784439));
#4677=DIRECTION('ref_axis',(0.866025403784439,0.,-0.5));
#4678=DIRECTION('',(0.,1.,0.));
#4679=DIRECTION('center_axis',(0.5,0.,0.866025403784439));
#4680=DIRECTION('ref_axis',(0.866025403784439,0.,-0.5));
#4681=DIRECTION('',(-0.866025403784439,0.,0.5));
#4682=DIRECTION('center_axis',(0.5,0.,0.866025403784439));
#4683=DIRECTION('ref_axis',(0.866025403784439,0.,-0.5));
#4684=DIRECTION('',(0.,-1.,0.));
#4685=DIRECTION('center_axis',(1.,0.,0.));
#4686=DIRECTION('ref_axis',(0.,0.,-1.));
#4687=DIRECTION('center_axis',(1.,0.,0.));
#4688=DIRECTION('ref_axis',(0.,0.,-1.));
#4689=DIRECTION('',(0.,0.,1.));
#4690=DIRECTION('center_axis',(1.,0.,0.));
#4691=DIRECTION('ref_axis',(0.,0.,-1.));
#4692=DIRECTION('',(0.,-1.,0.));
#4693=DIRECTION('center_axis',(1.,0.,0.));
#4694=DIRECTION('ref_axis',(0.,0.,-1.));
#4695=DIRECTION('',(0.,0.,-1.));
#4696=DIRECTION('center_axis',(1.,0.,0.));
#4697=DIRECTION('ref_axis',(0.,0.,-1.));
#4698=DIRECTION('',(0.,1.,0.));
#4699=DIRECTION('center_axis',(0.5,0.,-0.866025403784439));
#4700=DIRECTION('ref_axis',(-0.866025403784439,0.,-0.5));
#4701=DIRECTION('center_axis',(0.5,0.,-0.866025403784439));
#4702=DIRECTION('ref_axis',(-0.866025403784439,0.,-0.5));
#4703=DIRECTION('',(0.866025403784439,0.,0.5));
#4704=DIRECTION('center_axis',(0.5,0.,-0.866025403784439));
#4705=DIRECTION('ref_axis',(-0.866025403784439,0.,-0.5));
#4706=DIRECTION('',(0.,-1.,0.));
#4707=DIRECTION('center_axis',(0.5,0.,-0.866025403784439));
#4708=DIRECTION('ref_axis',(-0.866025403784439,0.,-0.5));
#4709=DIRECTION('',(-0.866025403784439,0.,-0.5));
#4710=DIRECTION('center_axis',(0.5,0.,-0.866025403784439));
#4711=DIRECTION('ref_axis',(-0.866025403784439,0.,-0.5));
#4712=DIRECTION('center_axis',(-0.5,0.,-0.866025403784439));
#4713=DIRECTION('ref_axis',(-0.866025403784439,0.,0.5));
#4714=DIRECTION('center_axis',(-0.5,0.,-0.866025403784439));
#4715=DIRECTION('ref_axis',(-0.866025403784439,0.,0.5));
#4716=DIRECTION('',(0.866025403784439,0.,-0.5));
#4717=DIRECTION('center_axis',(-0.5,0.,-0.866025403784439));
#4718=DIRECTION('ref_axis',(-0.866025403784439,0.,0.5));
#4719=DIRECTION('center_axis',(-0.5,0.,-0.866025403784439));
#4720=DIRECTION('ref_axis',(-0.866025403784439,0.,0.5));
#4721=DIRECTION('',(-0.866025403784439,0.,0.5));
#4722=DIRECTION('center_axis',(-0.5,0.,-0.866025403784439));
#4723=DIRECTION('ref_axis',(-0.866025403784439,0.,0.5));
#4724=DIRECTION('',(0.,1.,0.));
#4725=DIRECTION('center_axis',(0.,1.,0.));
#4726=DIRECTION('ref_axis',(0.,0.,1.));
#4727=DIRECTION('center_axis',(0.,-1.,0.));
#4728=DIRECTION('ref_axis',(8.88178419700125E-16,0.,1.));
#4729=DIRECTION('',(0.,0.,1.));
#4730=DIRECTION('center_axis',(0.,1.,0.));
#4731=DIRECTION('ref_axis',(0.,0.,1.));
#4732=DIRECTION('',(0.866025403784439,0.,0.5));
#4733=DIRECTION('',(0.866025403784439,0.,-0.5));
#4734=DIRECTION('center_axis',(0.,1.,0.));
#4735=DIRECTION('ref_axis',(0.,0.,1.));
#4736=DIRECTION('',(0.,0.,-1.));
#4737=DIRECTION('center_axis',(0.,1.,0.));
#4738=DIRECTION('ref_axis',(0.,0.,1.));
#4739=DIRECTION('',(-0.866025403784439,0.,-0.5));
#4740=DIRECTION('center_axis',(0.,1.,0.));
#4741=DIRECTION('ref_axis',(0.,0.,1.));
#4742=DIRECTION('',(-0.866025403784439,0.,0.5));
#4743=DIRECTION('center_axis',(0.,1.,0.));
#4744=DIRECTION('ref_axis',(0.,0.,1.));
#4745=DIRECTION('',(0.,0.,1.));
#4746=DIRECTION('center_axis',(0.,-1.,0.));
#4747=DIRECTION('ref_axis',(-8.88178419700125E-16,0.,1.));
#4748=DIRECTION('',(-0.866025403784439,0.,0.5));
#4749=DIRECTION('',(-0.866025403784439,0.,-0.5));
#4750=DIRECTION('center_axis',(0.,-1.,0.));
#4751=DIRECTION('ref_axis',(0.,0.,1.));
#4752=DIRECTION('',(0.,0.,-1.));
#4753=DIRECTION('center_axis',(0.,-1.,0.));
#4754=DIRECTION('ref_axis',(0.,0.,1.));
#4755=DIRECTION('',(0.866025403784439,0.,-0.5));
#4756=DIRECTION('center_axis',(0.,-1.,0.));
#4757=DIRECTION('ref_axis',(1.77635683940025E-15,0.,1.));
#4758=DIRECTION('',(0.866025403784439,0.,0.5));
#4759=DIRECTION('center_axis',(0.,-1.,0.));
#4760=DIRECTION('ref_axis',(0.,0.,1.));
#4761=DIRECTION('center_axis',(0.5,0.,0.866025403784438));
#4762=DIRECTION('ref_axis',(0.866025403784439,0.,-0.5));
#4763=DIRECTION('center_axis',(0.5,0.,-0.866025403784439));
#4764=DIRECTION('ref_axis',(-0.866025403784439,0.,-0.5));
#4765=DIRECTION('center_axis',(-0.5,0.,-0.866025403784439));
#4766=DIRECTION('ref_axis',(-0.866025403784439,0.,0.5));
#4767=DIRECTION('center_axis',(0.5,0.,0.866025403784438));
#4768=DIRECTION('ref_axis',(0.866025403784439,0.,-0.5));
#4769=DIRECTION('center_axis',(-0.5,0.,-0.866025403784439));
#4770=DIRECTION('ref_axis',(-0.866025403784439,0.,0.5));
#4771=DIRECTION('center_axis',(-1.,0.,0.));
#4772=DIRECTION('ref_axis',(0.,0.,1.));
#4773=DIRECTION('center_axis',(0.,-1.,0.));
#4774=DIRECTION('ref_axis',(0.,0.,-1.));
#4775=DIRECTION('center_axis',(0.5,0.,0.866025403784438));
#4776=DIRECTION('ref_axis',(0.866025403784439,0.,-0.5));
#4777=DIRECTION('center_axis',(-0.5,0.,0.866025403784439));
#4778=DIRECTION('ref_axis',(0.866025403784439,0.,0.5));
#4779=DIRECTION('center_axis',(0.5,0.,0.866025403784439));
#4780=DIRECTION('ref_axis',(0.866025403784439,0.,-0.5));
#4781=DIRECTION('center_axis',(0.,-1.,0.));
#4782=DIRECTION('ref_axis',(0.,0.,-1.));
#4783=DIRECTION('center_axis',(0.5,0.,0.866025403784438));
#4784=DIRECTION('ref_axis',(0.866025403784439,0.,-0.5));
#4785=DIRECTION('center_axis',(1.,0.,0.));
#4786=DIRECTION('ref_axis',(0.,0.,-1.));
#4787=DIRECTION('center_axis',(0.5,0.,0.866025403784439));
#4788=DIRECTION('ref_axis',(0.866025403784439,0.,-0.5));
#4789=DIRECTION('center_axis',(-0.5,0.,-0.866025403784439));
#4790=DIRECTION('ref_axis',(0.866025403784439,0.,-0.5));
#4791=DIRECTION('center_axis',(-0.5,0.,-0.866025403784439));
#4792=DIRECTION('ref_axis',(-0.866025403784439,0.,0.5));
#4793=DIRECTION('center_axis',(0.5,0.,-0.866025403784439));
#4794=DIRECTION('ref_axis',(-0.866025403784439,0.,-0.5));
#4795=DIRECTION('center_axis',(-0.5,0.,-0.866025403784439));
#4796=DIRECTION('ref_axis',(0.866025403784439,0.,-0.5));
#4797=DIRECTION('center_axis',(0.,1.,0.));
#4798=DIRECTION('ref_axis',(0.,0.,1.));
#4799=DIRECTION('center_axis',(-1.,0.,0.));
#4800=DIRECTION('ref_axis',(0.,0.,1.));
#4801=DIRECTION('center_axis',(-0.5,0.,-0.866025403784439));
#4802=DIRECTION('ref_axis',(-0.866025403784439,0.,0.5));
#4803=DIRECTION('center_axis',(-0.5,0.,-0.866025403784439));
#4804=DIRECTION('ref_axis',(0.866025403784439,0.,-0.5));
#4805=DIRECTION('center_axis',(0.,1.,0.));
#4806=DIRECTION('ref_axis',(0.,0.,1.));
#4807=DIRECTION('center_axis',(0.5,0.,0.866025403784439));
#4808=DIRECTION('ref_axis',(0.866025403784439,0.,-0.5));
#4809=DIRECTION('center_axis',(-0.5,0.,0.866025403784439));
#4810=DIRECTION('ref_axis',(0.866025403784439,0.,0.5));
#4811=DIRECTION('center_axis',(-0.5,0.,-0.866025403784439));
#4812=DIRECTION('ref_axis',(0.866025403784439,0.,-0.5));
#4813=DIRECTION('center_axis',(0.,1.,0.));
#4814=DIRECTION('ref_axis',(0.,0.,1.));
#4815=DIRECTION('center_axis',(1.,0.,0.));
#4816=DIRECTION('ref_axis',(0.,0.,-1.));
#4817=DIRECTION('center_axis',(0.5,0.,0.866025403784439));
#4818=DIRECTION('ref_axis',(0.866025403784439,0.,-0.5));
#4819=DIRECTION('center_axis',(0.,1.,0.));
#4820=DIRECTION('ref_axis',(1.,0.,0.));
#4821=DIRECTION('center_axis',(-5.17751283984664E-14,-0.1010864170244,0.994877648906221));
#4822=DIRECTION('ref_axis',(-4.05998175189893E-29,0.994877648906221,0.1010864170244));
#4823=DIRECTION('center_axis',(0.,-7.15573433840431E-14,-1.));
#4824=DIRECTION('ref_axis',(0.,-1.,7.15573433840431E-14));
#4825=DIRECTION('center_axis',(-0.199143465014893,0.,0.979970346664562));
#4826=DIRECTION('ref_axis',(-0.979970346664562,-8.67361737988404E-15,-0.199143465014893));
#4827=DIRECTION('center_axis',(0.,0.,1.));
#4828=DIRECTION('ref_axis',(1.,0.,0.));
#4829=DIRECTION('center_axis',(-7.15573433840431E-14,0.,-1.));
#4830=DIRECTION('ref_axis',(-1.,0.,7.15573433840431E-14));
#4831=DIRECTION('center_axis',(0.,1.,0.));
#4832=DIRECTION('ref_axis',(0.,0.,1.));
#4833=DIRECTION('center_axis',(-0.749107482659445,-7.02110417793331E-14,
0.662448473032906));
#4834=DIRECTION('ref_axis',(0.662448473032906,2.48599189023735E-28,0.749107482659445));
#4835=DIRECTION('center_axis',(0.5,0.,0.866025403784439));
#4836=DIRECTION('ref_axis',(0.866025403784439,0.,-0.5));
#4837=DIRECTION('center_axis',(0.829541231031753,-0.287196439203378,-0.478935853040076));
#4838=DIRECTION('ref_axis',(-0.5,4.17395137324621E-16,-0.866025403784439));
#4839=DIRECTION('center_axis',(-0.861589317610118,0.101086417024454,0.497438824453107));
#4840=DIRECTION('ref_axis',(0.5,-2.3942973477981E-18,0.866025403784439));
#4841=DIRECTION('center_axis',(1.,0.,0.));
#4842=DIRECTION('ref_axis',(0.,0.,-1.));
#4843=DIRECTION('center_axis',(0.,-0.287196439203358,0.957871706080158));
#4844=DIRECTION('ref_axis',(0.,-0.957871706080157,-0.287196439203358));
#4845=DIRECTION('center_axis',(1.,0.,0.));
#4846=DIRECTION('ref_axis',(0.,0.,-1.));
#4847=DIRECTION('center_axis',(0.,0.101086417024377,0.994877648906223));
#4848=DIRECTION('ref_axis',(0.,-0.994877648906223,0.101086417024377));
#4849=DIRECTION('center_axis',(-1.41253933285967E-14,-0.287196439203367,
-0.957871706080155));
#4850=DIRECTION('ref_axis',(7.2563925722977E-30,0.957871706080155,-0.287196439203367));
#4851=DIRECTION('center_axis',(0.,1.,0.));
#4852=DIRECTION('ref_axis',(1.,0.,0.));
#4853=DIRECTION('center_axis',(-0.199143465014904,2.93519296686958E-14,
-0.97997034666456));
#4854=DIRECTION('ref_axis',(0.97997034666456,-1.27881005982267E-29,-0.199143465014904));
#4855=DIRECTION('center_axis',(0.,1.,0.));
#4856=DIRECTION('ref_axis',(1.,0.,0.));
#4857=DIRECTION('center_axis',(-0.866025403784418,0.,0.500000000000037));
#4858=DIRECTION('ref_axis',(-0.500000000000037,0.,-0.866025403784418));
#4859=DIRECTION('center_axis',(0.,1.,0.));
#4860=DIRECTION('ref_axis',(1.,0.,0.));
#4861=DIRECTION('center_axis',(0.,-1.,0.));
#4862=DIRECTION('ref_axis',(-8.67361737988405E-15,0.,1.));
#4863=DIRECTION('center_axis',(0.,1.,0.));
#4864=DIRECTION('ref_axis',(1.,0.,0.));
#4865=DIRECTION('center_axis',(0.,-1.,1.00154306582477E-14));
#4866=DIRECTION('ref_axis',(-8.67361737988405E-15,1.00154306582477E-14,
1.));
#4867=DIRECTION('center_axis',(-0.829541231031753,0.28719643920338,-0.478935853040074));
#4868=DIRECTION('ref_axis',(0.499999999999998,-5.90524342983604E-16,-0.866025403784439));
#4869=DIRECTION('center_axis',(0.5,0.,-0.866025403784439));
#4870=DIRECTION('ref_axis',(-0.866025403784439,0.,-0.5));
#4871=DIRECTION('center_axis',(-0.861589317610107,0.101086417024411,-0.497438824453135));
#4872=DIRECTION('ref_axis',(-0.500000000000025,-2.05653966383454E-16,0.866025403784424));
#4873=DIRECTION('center_axis',(0.,1.,0.));
#4874=DIRECTION('ref_axis',(0.,0.,1.));
#4875=DIRECTION('center_axis',(-0.749107482659488,0.,-0.662448473032858));
#4876=DIRECTION('ref_axis',(-0.662448473032858,0.,0.749107482659488));
#4877=DIRECTION('center_axis',(-0.866025403784439,0.,0.5));
#4878=DIRECTION('ref_axis',(0.5,0.,0.866025403784439));
#4879=DIRECTION('center_axis',(-0.86602540378444,3.49641228577842E-14,0.499999999999998));
#4880=DIRECTION('ref_axis',(0.499999999999998,-4.11195107519449E-31,0.86602540378444));
#4881=DIRECTION('center_axis',(0.,-1.,0.));
#4882=DIRECTION('ref_axis',(0.,0.,-1.));
#4883=DIRECTION('center_axis',(0.,-1.,1.75270036519335E-14));
#4884=DIRECTION('ref_axis',(0.,-1.75270036519335E-14,-1.));
#4885=DIRECTION('center_axis',(1.,0.,0.));
#4886=DIRECTION('ref_axis',(0.,0.,-1.));
#4887=DIRECTION('center_axis',(0.,-0.101086417024342,-0.994877648906227));
#4888=DIRECTION('ref_axis',(0.,0.994877648906226,-0.101086417024342));
#4889=DIRECTION('center_axis',(-1.47481513352255E-14,0.287196439203365,
0.957871706080155));
#4890=DIRECTION('ref_axis',(2.65299810676557E-29,-0.957871706080155,0.287196439203365));
#4891=DIRECTION('center_axis',(0.,0.,-1.));
#4892=DIRECTION('ref_axis',(-1.,0.,0.));
#4893=DIRECTION('center_axis',(0.,-1.14925430283463E-13,-1.));
#4894=DIRECTION('ref_axis',(0.,1.,-1.14925430283463E-13));
#4895=DIRECTION('center_axis',(-1.14925430283463E-13,0.,1.));
#4896=DIRECTION('ref_axis',(1.,0.,1.14925430283463E-13));
#4897=DIRECTION('center_axis',(1.,0.,0.));
#4898=DIRECTION('ref_axis',(0.,0.,-1.));
#4899=DIRECTION('center_axis',(0.,0.287196439203363,-0.957871706080156));
#4900=DIRECTION('ref_axis',(0.,0.957871706080156,0.287196439203362));
#4901=DIRECTION('center_axis',(5.33981346144544E-14,-0.101086417024396,
0.994877648906221));
#4902=DIRECTION('ref_axis',(1.43307595785059E-29,-0.994877648906221,-0.101086417024396));
#4903=DIRECTION('center_axis',(0.,-1.,0.));
#4904=DIRECTION('ref_axis',(0.,0.,-1.));
#4905=DIRECTION('center_axis',(-9.75781955236951E-15,-1.,-5.63367974526431E-15));
#4906=DIRECTION('ref_axis',(1.,-9.75781955236951E-15,1.12103877145985E-44));
#4907=DIRECTION('center_axis',(0.,1.,0.));
#4908=DIRECTION('ref_axis',(1.,0.,0.));
#4909=DIRECTION('center_axis',(-0.866025403784439,-6.18356505287836E-14,
-0.5));
#4910=DIRECTION('ref_axis',(0.5,1.71607915375628E-30,-0.866025403784439));
#4911=DIRECTION('center_axis',(0.,1.,0.));
#4912=DIRECTION('ref_axis',(1.,0.,0.));
#4913=DIRECTION('center_axis',(-0.86158931761011,-0.101086417024435,0.497438824453126));
#4914=DIRECTION('ref_axis',(-0.500000000000016,-8.82954564193182E-15,-0.866025403784429));
#4915=DIRECTION('center_axis',(0.,1.,0.));
#4916=DIRECTION('ref_axis',(1.,0.,0.));
#4917=DIRECTION('center_axis',(-0.829541231031755,-0.287196439203371,0.478935853040076));
#4918=DIRECTION('ref_axis',(-0.499999999999996,-9.54243899220994E-15,-0.866025403784441));
#4919=DIRECTION('center_axis',(0.,1.,0.));
#4920=DIRECTION('ref_axis',(1.,0.,0.));
#4921=DIRECTION('center_axis',(-0.199143465014924,-4.21017614145968E-14,
0.979970346664556));
#4922=DIRECTION('ref_axis',(-0.979970346664556,-2.71050543121381E-15,-0.199143465014924));
#4923=DIRECTION('center_axis',(0.,1.,0.));
#4924=DIRECTION('ref_axis',(1.,0.,0.));
#4925=DIRECTION('center_axis',(-0.199143465014975,0.,-0.979970346664546));
#4926=DIRECTION('ref_axis',(0.979970346664546,3.52365706057789E-15,-0.199143465014975));
#4927=DIRECTION('center_axis',(0.,1.,0.));
#4928=DIRECTION('ref_axis',(1.,0.,0.));
#4929=DIRECTION('center_axis',(-0.829541231031756,-0.28719643920338,-0.478935853040069));
#4930=DIRECTION('ref_axis',(0.499999999999997,-1.39967667904725E-14,-0.86602540378444));
#4931=DIRECTION('center_axis',(0.866025403784439,0.,0.5));
#4932=DIRECTION('ref_axis',(0.5,0.,-0.866025403784439));
#4933=DIRECTION('center_axis',(-0.866025403784458,0.,-0.499999999999966));
#4934=DIRECTION('ref_axis',(-0.499999999999966,0.,0.866025403784458));
#4935=DIRECTION('center_axis',(-0.5,0.,0.866025403784439));
#4936=DIRECTION('ref_axis',(0.866025403784439,0.,0.5));
#4937=DIRECTION('center_axis',(0.829541231031765,-0.287196439203365,0.478935853040062));
#4938=DIRECTION('ref_axis',(0.499999999999983,-1.74562014011744E-16,-0.866025403784448));
#4939=DIRECTION('center_axis',(-0.861589317610119,0.101086417024448,-0.497438824453106));
#4940=DIRECTION('ref_axis',(-0.499999999999998,7.745902403892E-18,0.86602540378444));
#4941=DIRECTION('center_axis',(0.5,0.,0.866025403784439));
#4942=DIRECTION('ref_axis',(0.866025403784439,0.,-0.5));
#4943=DIRECTION('center_axis',(-0.829541231031758,-0.287196439203359,0.478935853040078));
#4944=DIRECTION('ref_axis',(0.499999999999999,2.51520075033803E-16,0.866025403784439));
#4945=DIRECTION('center_axis',(0.5,0.,0.866025403784439));
#4946=DIRECTION('ref_axis',(0.866025403784439,0.,-0.5));
#4947=DIRECTION('center_axis',(-0.861589317610127,-0.101086417024433,0.497438824453096));
#4948=DIRECTION('ref_axis',(0.499999999999987,8.21668458334066E-17,0.866025403784446));
#4949=DIRECTION('center_axis',(0.,1.,0.));
#4950=DIRECTION('ref_axis',(0.,0.,1.));
#4951=DIRECTION('center_axis',(-0.74910748265946,0.,0.662448473032889));
#4952=DIRECTION('ref_axis',(0.662448473032889,0.,0.74910748265946));
#4953=DIRECTION('center_axis',(0.,1.,0.));
#4954=DIRECTION('ref_axis',(0.,0.,1.));
#4955=DIRECTION('center_axis',(-0.749107482659464,5.54706567608847E-14,
-0.662448473032884));
#4956=DIRECTION('ref_axis',(-0.662448473032884,1.32414025723286E-28,0.749107482659464));
#4957=DIRECTION('center_axis',(0.5,0.,-0.866025403784439));
#4958=DIRECTION('ref_axis',(-0.866025403784439,0.,-0.5));
#4959=DIRECTION('center_axis',(-0.861589317610122,-0.101086417024408,-0.49743882445311));
#4960=DIRECTION('ref_axis',(-0.5,-7.15092813094045E-18,0.866025403784439));
#4961=DIRECTION('center_axis',(0.5,0.,-0.866025403784439));
#4962=DIRECTION('ref_axis',(-0.866025403784439,0.,-0.5));
#4963=DIRECTION('center_axis',(0.861589317610122,0.101086417024421,0.497438824453108));
#4964=DIRECTION('ref_axis',(0.499999999999998,7.16296697270556E-18,-0.86602540378444));
#4965=DIRECTION('center_axis',(-0.829541231031761,-0.287196439203368,-0.478935853040068));
#4966=DIRECTION('ref_axis',(-0.49999999999999,4.4460279883491E-16,0.866025403784444));
#4967=DIRECTION('center_axis',(0.,1.,0.));
#4968=DIRECTION('ref_axis',(1.,0.,0.));
#4969=DIRECTION('center_axis',(-0.948250947674409,3.63509986091514E-14,
-0.317521873631701));
#4970=DIRECTION('ref_axis',(0.317521873631701,-3.81262645548618E-29,-0.948250947674409));
#4971=DIRECTION('center_axis',(0.,1.,0.));
#4972=DIRECTION('ref_axis',(1.,0.,0.));
#4973=DIRECTION('center_axis',(-0.866025403784459,0.,-0.499999999999965));
#4974=DIRECTION('ref_axis',(0.499999999999965,0.,-0.866025403784459));
#4975=DIRECTION('center_axis',(6.1232339957368E-17,1.,0.));
#4976=DIRECTION('ref_axis',(1.,0.,0.));
#4977=DIRECTION('center_axis',(8.67361737988401E-15,-1.,5.00771532912383E-15));
#4978=DIRECTION('ref_axis',(-1.,-8.67361737988387E-15,2.60208521396521E-14));
#4979=DIRECTION('center_axis',(0.,1.,0.));
#4980=DIRECTION('ref_axis',(1.,0.,0.));
#4981=DIRECTION('center_axis',(-0.866025403784439,3.43831006646852E-14,
0.5));
#4982=DIRECTION('ref_axis',(-0.5,2.49525696807541E-30,-0.866025403784439));
#4983=DIRECTION('center_axis',(0.,1.,0.));
#4984=DIRECTION('ref_axis',(1.,0.,0.));
#4985=DIRECTION('center_axis',(-0.866025403784404,0.,-0.500000000000061));
#4986=DIRECTION('ref_axis',(0.500000000000061,0.,-0.866025403784404));
#4987=DIRECTION('center_axis',(6.1232339957368E-17,1.,0.));
#4988=DIRECTION('ref_axis',(1.,0.,0.));
#4989=DIRECTION('center_axis',(-0.829541231031754,0.287196439203375,0.478935853040075));
#4990=DIRECTION('ref_axis',(-0.499999999999992,2.58221544109979E-14,-0.866025403784443));
#4991=DIRECTION('center_axis',(-0.5,0.,-0.866025403784439));
#4992=DIRECTION('ref_axis',(-0.866025403784439,0.,0.5));
#4993=DIRECTION('center_axis',(-0.86158931761011,0.101086417024435,0.497438824453126));
#4994=DIRECTION('ref_axis',(0.500000000000017,-2.46607843488102E-16,0.866025403784429));
#4995=DIRECTION('center_axis',(0.,1.,0.));
#4996=DIRECTION('ref_axis',(1.22464679914735E-16,0.,-1.));
#4997=DIRECTION('center_axis',(-0.948250947674425,0.,0.317521873631651));
#4998=DIRECTION('ref_axis',(0.317521873631651,0.,0.948250947674425));
#4999=DIRECTION('center_axis',(0.,1.,0.));
#5000=DIRECTION('ref_axis',(0.,0.,1.));
#5001=DIRECTION('center_axis',(0.749107482659426,0.,0.662448473032928));
#5002=DIRECTION('ref_axis',(0.662448473032928,0.,-0.749107482659426));
#5003=DIRECTION('center_axis',(-0.199143465014904,-2.93519296686958E-14,
-0.97997034666456));
#5004=DIRECTION('ref_axis',(-0.97997034666456,-1.27881005982267E-29,0.199143465014904));
#5005=DIRECTION('center_axis',(-0.866025403784439,0.,-0.5));
#5006=DIRECTION('ref_axis',(-0.5,0.,0.866025403784439));
#5007=DIRECTION('center_axis',(-0.866025403784439,4.6812504541412E-14,-0.5));
#5008=DIRECTION('ref_axis',(-0.5,5.19337291326334E-30,0.866025403784439));
#5009=DIRECTION('center_axis',(0.,-1.,0.));
#5010=DIRECTION('ref_axis',(-1.65389215948552E-15,0.,1.));
#5011=DIRECTION('center_axis',(-9.75781955236951E-15,-1.,5.63367974526431E-15));
#5012=DIRECTION('ref_axis',(1.,-9.75781955236951E-15,-1.68155815718978E-43));
#5013=DIRECTION('center_axis',(0.5,0.,0.866025403784439));
#5014=DIRECTION('ref_axis',(0.866025403784439,0.,-0.5));
#5015=DIRECTION('center_axis',(0.861589317610114,-0.101086417024512,-0.497438824453103));
#5016=DIRECTION('ref_axis',(-0.499999999999998,6.37095659320221E-18,-0.86602540378444));
#5017=DIRECTION('center_axis',(-0.829541231031761,0.287196439203367,0.478935853040068));
#5018=DIRECTION('ref_axis',(0.49999999999999,4.16045429843481E-16,0.866025403784444));
#5019=DIRECTION('center_axis',(0.866025403784439,0.,-0.5));
#5020=DIRECTION('ref_axis',(-0.5,0.,-0.866025403784439));
#5021=DIRECTION('center_axis',(-0.866025403784432,0.,0.500000000000011));
#5022=DIRECTION('ref_axis',(0.500000000000011,0.,0.866025403784432));
#5023=DIRECTION('center_axis',(-0.866025403784439,0.,-0.5));
#5024=DIRECTION('ref_axis',(-0.5,0.,0.866025403784439));
#5025=DIRECTION('center_axis',(-0.86602540378444,-7.18061389639901E-14,
-0.499999999999998));
#5026=DIRECTION('ref_axis',(-0.499999999999998,-1.36530950454694E-29,0.86602540378444));
#5027=DIRECTION('center_axis',(0.5,0.,-0.866025403784439));
#5028=DIRECTION('ref_axis',(-0.866025403784439,0.,-0.5));
#5029=DIRECTION('center_axis',(-0.829541231031757,0.287196439203362,-0.478935853040077));
#5030=DIRECTION('ref_axis',(-0.499999999999999,2.55714797234654E-16,0.866025403784439));
#5031=DIRECTION('center_axis',(0.861589317610141,-0.101086417024404,0.497438824453078));
#5032=DIRECTION('ref_axis',(0.499999999999968,3.57293483672415E-18,-0.866025403784457));
#5033=DIRECTION('center_axis',(0.,1.,0.));
#5034=DIRECTION('ref_axis',(1.,0.,0.));
#5035=DIRECTION('center_axis',(-0.86602540378444,-3.49641228577842E-14,
0.499999999999998));
#5036=DIRECTION('ref_axis',(-0.499999999999998,-4.11195107519449E-31,-0.86602540378444));
#5037=DIRECTION('center_axis',(0.,1.,0.));
#5038=DIRECTION('ref_axis',(-0.994979986397824,0.,-0.100074105880518));
#5039=DIRECTION('center_axis',(0.,-0.101086417024377,0.994877648906223));
#5040=DIRECTION('ref_axis',(-8.673617379884E-15,0.994877648906223,0.101086417024377));
#5041=DIRECTION('center_axis',(-7.15573433840431E-14,0.,-1.));
#5042=DIRECTION('ref_axis',(1.,0.,-7.15573433840431E-14));
#5043=DIRECTION('center_axis',(0.,1.,0.));
#5044=DIRECTION('ref_axis',(1.,0.,0.));
#5045=DIRECTION('center_axis',(-0.861589317610132,-0.101086417024438,-0.497438824453087));
#5046=DIRECTION('ref_axis',(0.499999999999978,-2.08058901956142E-16,-0.866025403784451));
#5047=DIRECTION('center_axis',(6.12323399573678E-17,1.,0.));
#5048=DIRECTION('ref_axis',(1.,0.,0.));
#5049=DIRECTION('center_axis',(-0.82954123103176,-0.287196439203352,-0.478935853040079));
#5050=DIRECTION('ref_axis',(0.499999999999995,1.40437046887256E-14,-0.866025403784441));
#5051=DIRECTION('center_axis',(0.,1.,0.));
#5052=DIRECTION('ref_axis',(1.,0.,0.));
#5053=DIRECTION('center_axis',(0.,1.,0.));
#5054=DIRECTION('ref_axis',(1.,0.,0.));
#5055=DIRECTION('center_axis',(-0.948250947674411,0.,-0.317521873631694));
#5056=DIRECTION('ref_axis',(0.317521873631694,1.24683249835833E-14,-0.948250947674411));
#5057=DIRECTION('center_axis',(6.12323399573678E-17,1.,0.));
#5058=DIRECTION('ref_axis',(1.,0.,0.));
#5059=DIRECTION('center_axis',(-0.829541231031755,-0.287196439203371,0.478935853040075));
#5060=DIRECTION('ref_axis',(-0.499999999999998,-1.76231351345845E-16,-0.86602540378444));
#5061=DIRECTION('center_axis',(0.866025403784439,0.,-0.5));
#5062=DIRECTION('ref_axis',(-0.5,0.,-0.866025403784439));
#5063=DIRECTION('center_axis',(-0.864858564672233,-0.0505745605773519,0.499461587046984));
#5064=DIRECTION('ref_axis',(-0.500089321311808,-0.000278942162528612,-0.865973783033392));
#5065=DIRECTION('center_axis',(0.,0.,-1.));
#5066=DIRECTION('ref_axis',(-1.,0.,0.));
#5067=DIRECTION('center_axis',(0.000117146476148524,-0.0505745644176246,
-0.998720281014995));
#5068=DIRECTION('ref_axis',(-0.446156523227928,0.893807017247891,-0.0453141556204722));
#5069=DIRECTION('center_axis',(-1.,0.,0.));
#5070=DIRECTION('ref_axis',(0.,0.,1.));
#5071=DIRECTION('center_axis',(1.99425739796376E-14,-0.287196439203364,
0.957871706080156));
#5072=DIRECTION('ref_axis',(-1.63640921780907E-29,-0.957871706080156,-0.287196439203364));
#5073=DIRECTION('center_axis',(-0.5,0.,0.866025403784439));
#5074=DIRECTION('ref_axis',(0.866025403784439,0.,0.5));
#5075=DIRECTION('center_axis',(-0.829541231031752,-0.287196439203385,-0.478935853040072));
#5076=DIRECTION('ref_axis',(-0.499999999999997,1.26305293957536E-17,0.866025403784441));
#5077=DIRECTION('center_axis',(-0.5,0.,0.866025403784439));
#5078=DIRECTION('ref_axis',(0.866025403784439,0.,0.5));
#5079=DIRECTION('center_axis',(-0.861589317610078,-0.101086417024462,-0.497438824453176));
#5080=DIRECTION('ref_axis',(-0.500000000000069,4.95586472996822E-17,0.866025403784399));
#5081=DIRECTION('center_axis',(0.,1.,0.));
#5082=DIRECTION('ref_axis',(1.01064309961486E-15,0.,-1.));
#5083=DIRECTION('center_axis',(-0.948250947674425,6.51376792599937E-14,
0.317521873631651));
#5084=DIRECTION('ref_axis',(0.317521873631651,-1.16313243025547E-28,0.948250947674425));
#5085=DIRECTION('center_axis',(-0.5,0.,-0.866025403784439));
#5086=DIRECTION('ref_axis',(-0.866025403784439,0.,0.5));
#5087=DIRECTION('center_axis',(-0.861589317610114,-0.101086417024508,0.497438824453103));
#5088=DIRECTION('ref_axis',(0.499999999999998,6.17150082144409E-18,0.86602540378444));
#5089=DIRECTION('center_axis',(-0.5,0.,-0.866025403784439));
#5090=DIRECTION('ref_axis',(-0.866025403784439,0.,0.5));
#5091=DIRECTION('center_axis',(-0.829541231031752,-0.287196439203378,0.478935853040076));
#5092=DIRECTION('ref_axis',(0.5,5.39313107558868E-16,0.866025403784438));
#5093=DIRECTION('center_axis',(-1.,0.,0.));
#5094=DIRECTION('ref_axis',(0.,0.,1.));
#5095=DIRECTION('center_axis',(0.,-0.287196439203354,-0.957871706080159));
#5096=DIRECTION('ref_axis',(0.,0.957871706080159,-0.287196439203354));
#5097=DIRECTION('center_axis',(0.,1.,0.));
#5098=DIRECTION('ref_axis',(1.,0.,0.));
#5099=DIRECTION('center_axis',(0.,-1.,-2.00308613164954E-14));
#5100=DIRECTION('ref_axis',(0.,-2.00308613164954E-14,1.));
#5101=DIRECTION('center_axis',(0.,1.,0.));
#5102=DIRECTION('ref_axis',(1.,0.,0.));
#5103=DIRECTION('center_axis',(-0.86602540378444,-3.1747643037438E-15,-0.499999999999998));
#5104=DIRECTION('ref_axis',(0.499999999999998,5.34273510922176E-31,-0.86602540378444));
#5105=DIRECTION('center_axis',(0.,1.,0.));
#5106=DIRECTION('ref_axis',(1.,0.,0.));
#5107=DIRECTION('center_axis',(-0.866025403784432,0.,0.500000000000011));
#5108=DIRECTION('ref_axis',(-0.500000000000011,0.,-0.866025403784432));
#5109=DIRECTION('center_axis',(0.,1.,0.));
#5110=DIRECTION('ref_axis',(-0.866025403784434,0.,-0.500000000000007));
#5111=DIRECTION('center_axis',(-8.67361737988407E-15,-1.,5.00771532912386E-15));
#5112=DIRECTION('ref_axis',(-1.,8.67361737988407E-15,-2.69049305150365E-43));
#5113=DIRECTION('center_axis',(0.,-1.,0.));
#5114=DIRECTION('ref_axis',(0.,0.,-1.));
#5115=DIRECTION('center_axis',(5.42101086242751E-15,-1.,3.12982208070238E-15));
#5116=DIRECTION('ref_axis',(1.,5.42101086242751E-15,0.));
#5117=DIRECTION('center_axis',(-0.5,0.,0.866025403784439));
#5118=DIRECTION('ref_axis',(0.866025403784439,0.,0.5));
#5119=DIRECTION('center_axis',(0.861589317610118,-0.101086417024453,0.497438824453107));
#5120=DIRECTION('ref_axis',(0.5,-7.47725293442112E-18,-0.866025403784439));
#5121=DIRECTION('center_axis',(-0.829541231031759,0.287196439203384,-0.478935853040061));
#5122=DIRECTION('ref_axis',(-0.499999999999986,-7.38722988415026E-16,0.866025403784447));
#5123=DIRECTION('center_axis',(0.866025403784439,0.,0.5));
#5124=DIRECTION('ref_axis',(0.5,0.,-0.866025403784439));
#5125=DIRECTION('center_axis',(-0.866025403784437,0.,-0.500000000000003));
#5126=DIRECTION('ref_axis',(-0.500000000000003,0.,0.866025403784437));
#5127=DIRECTION('center_axis',(-0.866025403784439,0.,0.5));
#5128=DIRECTION('ref_axis',(0.5,0.,0.866025403784439));
#5129=DIRECTION('center_axis',(-0.866025403784439,-3.43831006646852E-14,
0.5));
#5130=DIRECTION('ref_axis',(0.5,2.49525696807541E-30,0.866025403784439));
#5131=DIRECTION('center_axis',(-0.5,0.,-0.866025403784439));
#5132=DIRECTION('ref_axis',(-0.866025403784439,0.,0.5));
#5133=DIRECTION('center_axis',(-0.829541231031752,0.287196439203382,0.478935853040074));
#5134=DIRECTION('ref_axis',(0.499999999999998,-5.7450135142724E-16,0.866025403784439));
#5135=DIRECTION('center_axis',(0.861589317610127,-0.101086417024433,-0.497438824453096));
#5136=DIRECTION('ref_axis',(-0.499999999999987,8.21668458334066E-17,-0.866025403784446));
#5137=DIRECTION('center_axis',(0.,-1.,0.));
#5138=DIRECTION('ref_axis',(0.,0.,-1.));
#5139=DIRECTION('center_axis',(0.,-1.,-1.12673594905287E-14));
#5140=DIRECTION('ref_axis',(0.,1.12673594905287E-14,-1.));
#5141=DIRECTION('center_axis',(0.,1.,0.));
#5142=DIRECTION('ref_axis',(1.,0.,0.));
#5143=DIRECTION('center_axis',(0.,-0.287196439203347,-0.957871706080161));
#5144=DIRECTION('ref_axis',(-8.67361737988404E-15,-0.957871706080161,0.287196439203347));
#5145=DIRECTION('center_axis',(0.,1.,0.));
#5146=DIRECTION('ref_axis',(1.,0.,0.));
#5147=DIRECTION('center_axis',(-0.749107482659497,-3.02324171289191E-14,
-0.662448473032847));
#5148=DIRECTION('ref_axis',(0.662448473032847,1.76182853028899E-15,-0.749107482659497));
#5149=DIRECTION('center_axis',(0.,1.,0.));
#5150=DIRECTION('ref_axis',(1.,0.,0.));
#5151=DIRECTION('center_axis',(-0.74910748265946,0.,0.662448473032889));
#5152=DIRECTION('ref_axis',(-0.662448473032889,1.76182853028895E-15,-0.74910748265946));
#5153=DIRECTION('center_axis',(0.,1.,0.));
#5154=DIRECTION('ref_axis',(1.,0.,0.));
#5155=DIRECTION('center_axis',(-1.95250156806324E-14,-0.287196439203363,
0.957871706080156));
#5156=DIRECTION('ref_axis',(-4.61450960908913E-30,0.957871706080156,0.287196439203363));
#5157=DIRECTION('center_axis',(-1.,0.,0.));
#5158=DIRECTION('ref_axis',(0.,0.,1.));
#5159=DIRECTION('center_axis',(-5.33981346144544E-14,-0.101086417024396,
-0.994877648906221));
#5160=DIRECTION('ref_axis',(1.35459394958056E-29,0.994877648906221,-0.101086417024396));
#5161=DIRECTION('center_axis',(0.,1.,0.));
#5162=DIRECTION('ref_axis',(0.,0.,1.));
#5163=DIRECTION('center_axis',(-0.199143465014975,0.,-0.979970346664546));
#5164=DIRECTION('ref_axis',(-0.979970346664546,0.,0.199143465014975));
#5165=DIRECTION('center_axis',(0.,1.,0.));
#5166=DIRECTION('ref_axis',(0.,0.,1.));
#5167=DIRECTION('center_axis',(-0.199143465014928,4.4226733372247E-14,0.979970346664555));
#5168=DIRECTION('ref_axis',(0.979970346664555,-4.97863136211578E-29,0.199143465014928));
#5169=DIRECTION('center_axis',(-1.,0.,0.));
#5170=DIRECTION('ref_axis',(0.,0.,1.));
#5171=DIRECTION('center_axis',(0.,-0.101086417024344,0.994877648906226));
#5172=DIRECTION('ref_axis',(0.,-0.994877648906226,-0.101086417024344));
#5173=DIRECTION('center_axis',(0.,1.,0.));
#5174=DIRECTION('ref_axis',(1.,0.,0.));
#5175=DIRECTION('center_axis',(0.,1.14925430283463E-13,-1.));
#5176=DIRECTION('ref_axis',(0.,-1.,-1.14925430283463E-13));
#5177=DIRECTION('center_axis',(0.,1.,0.));
#5178=DIRECTION('ref_axis',(-0.994979986397858,0.,-0.100074105880182));
#5179=DIRECTION('center_axis',(-1.14925430283463E-13,0.,1.));
#5180=DIRECTION('ref_axis',(-1.,0.,-1.14925430283463E-13));
#5181=DIRECTION('center_axis',(0.,0.,1.));
#5182=DIRECTION('ref_axis',(1.,0.,0.));
#5183=DIRECTION('center_axis',(0.,-1.,0.));
#5184=DIRECTION('ref_axis',(0.,0.,-1.));
#7892=CARTESIAN_POINT('',(0.,0.,0.));
#7893=CARTESIAN_POINT('Origin',(0.,0.2,0.));
#7894=CARTESIAN_POINT('',(-1.40834381901946E-16,0.2,1.15));
#7895=CARTESIAN_POINT('Origin',(0.,0.2,0.));
#7896=CARTESIAN_POINT('',(-1.65327317884893E-16,-1.04083408558608E-16,1.35));
#7897=CARTESIAN_POINT('',(-1.40834381901946E-16,0.2,1.15));
#7898=CARTESIAN_POINT('Origin',(0.,0.,0.));
#7899=CARTESIAN_POINT('Origin',(0.,4.85,0.));
#7900=CARTESIAN_POINT('',(-1.40834381901946E-16,4.85,1.15));
#7901=CARTESIAN_POINT('Origin',(0.,4.85,0.));
#7902=CARTESIAN_POINT('',(-1.40834381901946E-16,4.85,1.15));
#7903=CARTESIAN_POINT('Origin',(0.,0.0499999999999997,0.));
#7904=CARTESIAN_POINT('',(0.858631047345558,0.,2.56422556038549));
#7905=CARTESIAN_POINT('',(-0.858631047345558,0.,2.56422556038549));
#7906=CARTESIAN_POINT('Origin',(0.,0.,0.));
#7907=CARTESIAN_POINT('',(0.865846434298039,0.00546218487394905,2.58577367433831));
#7908=CARTESIAN_POINT('Origin',(0.858631047345555,0.0499999999999995,2.56422556038549));
#7909=CARTESIAN_POINT('',(-0.865846434298039,0.00546218487394904,2.58577367433831));
#7910=CARTESIAN_POINT('Origin',(0.,0.00546218487394896,0.));
#7911=CARTESIAN_POINT('Origin',(-0.858631047345558,0.05,2.56422556038549));
#7912=CARTESIAN_POINT('Origin',(2.16840434497101E-16,2.45,-3.05995642670502));
#7913=CARTESIAN_POINT('',(-0.025,2.20285867594495,-3.10325769689424));
#7914=CARTESIAN_POINT('',(0.0250000000000005,2.20285867594495,-3.10325769689424));
#7915=CARTESIAN_POINT('Origin',(4.60785923306339E-16,2.20285867594495,-3.05995642670502));
#7916=CARTESIAN_POINT('',(0.0250000000000005,0.247141324055048,-3.10325769689424));
#7917=CARTESIAN_POINT('',(0.0250000000000005,2.45,-3.10325769689424));
#7918=CARTESIAN_POINT('',(-0.025,0.247141324055048,-3.10325769689424));
#7919=CARTESIAN_POINT('Origin',(-1.01643953670516E-17,0.247141324055048,
-3.05995642670502));
#7920=CARTESIAN_POINT('',(-0.0250000000000001,2.45,-3.10325769689424));
#7921=CARTESIAN_POINT('Origin',(0.,2.4,0.));
#7922=CARTESIAN_POINT('',(0.865846434298034,2.44453781512605,2.58577367433831));
#7923=CARTESIAN_POINT('',(-0.865846434298034,2.44453781512605,2.58577367433831));
#7924=CARTESIAN_POINT('Origin',(0.,2.44453781512605,0.));
#7925=CARTESIAN_POINT('',(0.858631047345553,2.45,2.56422556038549));
#7926=CARTESIAN_POINT('Origin',(0.858631047345553,2.4,2.56422556038549));
#7927=CARTESIAN_POINT('',(-0.858631047345553,2.45,2.56422556038549));
#7928=CARTESIAN_POINT('Origin',(0.,2.45,0.));
#7929=CARTESIAN_POINT('Origin',(-0.85863104734555,2.4,2.56422556038549));
#7930=CARTESIAN_POINT('Origin',(0.,3.025,0.));
#7931=CARTESIAN_POINT('',(3.09223316784707E-16,3.025,2.525));
#7932=CARTESIAN_POINT('Origin',(0.,3.025,0.));
#7933=CARTESIAN_POINT('',(1.8934467256106E-32,5.55,1.54611658392353E-16));
#7934=CARTESIAN_POINT('Origin',(0.,3.025,0.));
#7935=CARTESIAN_POINT('Origin',(0.,5.55,0.));
#7936=CARTESIAN_POINT('',(-3.09223316784707E-16,2.45,2.525));
#7937=CARTESIAN_POINT('Origin',(0.,2.45,0.));
#7938=CARTESIAN_POINT('',(-3.09223316784707E-16,5.55,2.525));
#7939=CARTESIAN_POINT('Origin',(0.,5.35,0.));
#7940=CARTESIAN_POINT('',(-2.67226890756303,0.00546218487394984,0.543041829290872));
#7941=CARTESIAN_POINT('',(-1.80642247326498,0.00546218487394976,2.04273184504743));
#7942=CARTESIAN_POINT('Origin',(0.,0.00546218487394983,0.));
#7943=CARTESIAN_POINT('',(-2.67226890756303,0.204260158710973,1.54283517312858));
#7944=CARTESIAN_POINT('Origin',(-1.33613445378151,5.35,2.31425275969287));
#7945=CARTESIAN_POINT('Origin',(-2.67226890756303,5.35,0.));
#7946=CARTESIAN_POINT('Origin',(0.,5.35,0.));
#7947=CARTESIAN_POINT('',(2.67226890756303,0.00546218487394984,-0.543041829290872));
#7948=CARTESIAN_POINT('',(1.80642247326498,0.00546218487394912,-2.04273184504743));
#7949=CARTESIAN_POINT('Origin',(0.,0.00546218487394983,0.));
#7950=CARTESIAN_POINT('',(2.67226890756303,0.204260158710974,-1.54283517312858));
#7951=CARTESIAN_POINT('Origin',(1.33613445378151,5.35,-2.31425275969287));
#7952=CARTESIAN_POINT('Origin',(2.67226890756303,5.35,0.));
#7953=CARTESIAN_POINT('Origin',(0.,-2.9,0.));
#7954=CARTESIAN_POINT('',(-1.80642247326499,2.44453781512605,2.04273184504743));
#7955=CARTESIAN_POINT('',(-2.67226890756303,2.44453781512605,0.543041829290881));
#7956=CARTESIAN_POINT('Origin',(0.,2.44453781512605,0.));
#7957=CARTESIAN_POINT('',(-2.67226890756303,2.24573984128903,1.54283517312858));
#7958=CARTESIAN_POINT('Origin',(-2.67226890756303,-2.9,0.));
#7959=CARTESIAN_POINT('Origin',(-1.33613445378151,-2.9,2.31425275969287));
#7960=CARTESIAN_POINT('Origin',(0.,-2.9,0.));
#7961=CARTESIAN_POINT('',(1.80642247326499,2.44453781512605,-2.04273184504743));
#7962=CARTESIAN_POINT('',(2.67226890756303,2.44453781512605,-0.543041829290881));
#7963=CARTESIAN_POINT('Origin',(0.,2.44453781512605,0.));
#7964=CARTESIAN_POINT('',(2.67226890756303,2.24573984128903,-1.54283517312858));
#7965=CARTESIAN_POINT('Origin',(2.67226890756303,-2.9,0.));
#7966=CARTESIAN_POINT('Origin',(1.33613445378151,-2.9,-2.31425275969287));
#7967=CARTESIAN_POINT('Origin',(-2.7,2.45,0.));
#7968=CARTESIAN_POINT('',(-2.7,2.20285867594495,-1.52997821335251));
#7969=CARTESIAN_POINT('',(-2.7,0.247141324055048,-1.52997821335251));
#7970=CARTESIAN_POINT('',(-2.7,2.45,-1.52997821335251));
#7971=CARTESIAN_POINT('',(-2.7,0.05,-0.538516480713451));
#7972=CARTESIAN_POINT('Origin',(-2.7,5.35,0.));
#7973=CARTESIAN_POINT('',(-2.7,0.05,0.538516480713451));
#7974=CARTESIAN_POINT('',(-2.7,0.05,0.295803989154973));
#7975=CARTESIAN_POINT('',(-2.7,0.247141324055048,1.52997821335251));
#7976=CARTESIAN_POINT('Origin',(-2.7,5.35,0.));
#7977=CARTESIAN_POINT('',(-2.7,2.20285867594495,1.52997821335251));
#7978=CARTESIAN_POINT('',(-2.7,2.45,1.52997821335251));
#7979=CARTESIAN_POINT('',(-2.7,2.4,0.538516480713459));
#7980=CARTESIAN_POINT('Origin',(-2.7,-2.9,0.));
#7981=CARTESIAN_POINT('',(-2.7,2.4,-0.538516480713458));
#7982=CARTESIAN_POINT('',(-2.7,2.4,0.));
#7983=CARTESIAN_POINT('Origin',(-2.7,-2.9,0.));
#7984=CARTESIAN_POINT('Origin',(-1.35,2.45,2.33826859021798));
#7985=CARTESIAN_POINT('',(-2.675,0.247141324055048,1.57327948354173));
#7986=CARTESIAN_POINT('',(-1.81636895265444,0.0499999999999984,2.06901034986126));
#7987=CARTESIAN_POINT('Origin',(-1.35,5.35,2.33826859021798));
#7988=CARTESIAN_POINT('',(-0.883631047345559,0.0499999999999988,2.60752683057471));
#7989=CARTESIAN_POINT('',(-1.09382623085102,0.05,2.48617058479547));
#7990=CARTESIAN_POINT('',(-0.025,0.247141324055048,3.10325769689424));
#7991=CARTESIAN_POINT('Origin',(-1.35,5.35,2.33826859021798));
#7992=CARTESIAN_POINT('',(-0.025,2.20285867594495,3.10325769689424));
#7993=CARTESIAN_POINT('',(-0.0250000000000001,2.45,3.10325769689424));
#7994=CARTESIAN_POINT('',(-0.883631047345551,2.4,2.60752683057471));
#7995=CARTESIAN_POINT('Origin',(-1.35,-2.9,2.33826859021798));
#7996=CARTESIAN_POINT('',(-1.81636895265445,2.4,2.06901034986126));
#7997=CARTESIAN_POINT('',(-1.35,2.4,2.33826859021798));
#7998=CARTESIAN_POINT('',(-2.675,2.20285867594495,1.57327948354173));
#7999=CARTESIAN_POINT('Origin',(-1.35,-2.9,2.33826859021798));
#8000=CARTESIAN_POINT('',(-2.675,2.45,1.57327948354173));
#8001=CARTESIAN_POINT('Origin',(1.35,2.45,2.33826859021798));
#8002=CARTESIAN_POINT('',(0.0250000000000002,0.247141324055048,3.10325769689424));
#8003=CARTESIAN_POINT('',(0.883631047345559,0.0499999999999988,2.60752683057471));
#8004=CARTESIAN_POINT('Origin',(1.35,5.35,2.33826859021798));
#8005=CARTESIAN_POINT('',(1.81636895265444,0.0499999999999985,2.06901034986126));
#8006=CARTESIAN_POINT('',(1.60617376914898,0.05,2.1903665956405));
#8007=CARTESIAN_POINT('',(2.675,0.247141324055048,1.57327948354173));
#8008=CARTESIAN_POINT('Origin',(1.35,5.35,2.33826859021798));
#8009=CARTESIAN_POINT('',(2.675,2.20285867594495,1.57327948354173));
#8010=CARTESIAN_POINT('',(2.675,2.45,1.57327948354173));
#8011=CARTESIAN_POINT('',(1.81636895265445,2.4,2.06901034986126));
#8012=CARTESIAN_POINT('Origin',(1.35,-2.9,2.33826859021798));
#8013=CARTESIAN_POINT('',(0.883631047345552,2.4,2.60752683057471));
#8014=CARTESIAN_POINT('',(1.35,2.4,2.33826859021798));
#8015=CARTESIAN_POINT('',(0.0250000000000002,2.20285867594495,3.10325769689424));
#8016=CARTESIAN_POINT('Origin',(1.35,-2.9,2.33826859021798));
#8017=CARTESIAN_POINT('',(0.0250000000000003,2.45,3.10325769689424));
#8018=CARTESIAN_POINT('Origin',(2.7,2.45,0.));
#8019=CARTESIAN_POINT('',(2.7,2.20285867594495,-1.52997821335251));
#8020=CARTESIAN_POINT('',(2.7,2.4,-0.538516480713459));
#8021=CARTESIAN_POINT('Origin',(2.7,-2.9,0.));
#8022=CARTESIAN_POINT('',(2.7,2.4,0.538516480713459));
#8023=CARTESIAN_POINT('',(2.7,2.4,0.));
#8024=CARTESIAN_POINT('',(2.7,2.20285867594495,1.52997821335251));
#8025=CARTESIAN_POINT('Origin',(2.7,-2.9,0.));
#8026=CARTESIAN_POINT('',(2.7,0.247141324055047,1.52997821335251));
#8027=CARTESIAN_POINT('',(2.7,2.45,1.52997821335251));
#8028=CARTESIAN_POINT('',(2.7,0.05,0.538516480713451));
#8029=CARTESIAN_POINT('Origin',(2.7,5.35,0.));
#8030=CARTESIAN_POINT('',(2.7,0.05,-0.538516480713451));
#8031=CARTESIAN_POINT('',(2.7,0.05,-0.295803989154973));
#8032=CARTESIAN_POINT('',(2.7,0.247141324055048,-1.52997821335251));
#8033=CARTESIAN_POINT('Origin',(2.7,5.35,0.));
#8034=CARTESIAN_POINT('',(2.7,2.45,-1.52997821335251));
#8035=CARTESIAN_POINT('Origin',(1.35,2.45,-2.33826859021798));
#8036=CARTESIAN_POINT('',(0.883631047345552,2.4,-2.60752683057471));
#8037=CARTESIAN_POINT('Origin',(1.35,-2.9,-2.33826859021798));
#8038=CARTESIAN_POINT('',(1.81636895265445,2.4,-2.06901034986126));
#8039=CARTESIAN_POINT('',(1.35,2.4,-2.33826859021798));
#8040=CARTESIAN_POINT('',(2.675,2.20285867594495,-1.57327948354173));
#8041=CARTESIAN_POINT('Origin',(1.35,-2.9,-2.33826859021798));
#8042=CARTESIAN_POINT('',(2.675,0.247141324055048,-1.57327948354173));
#8043=CARTESIAN_POINT('',(2.675,2.45,-1.57327948354173));
#8044=CARTESIAN_POINT('',(1.81636895265444,0.0499999999999992,-2.06901034986126));
#8045=CARTESIAN_POINT('Origin',(1.35,5.35,-2.33826859021798));
#8046=CARTESIAN_POINT('',(0.883631047345561,0.0499999999999995,-2.60752683057471));
#8047=CARTESIAN_POINT('',(1.09382623085102,0.05,-2.48617058479547));
#8048=CARTESIAN_POINT('Origin',(1.35,5.35,-2.33826859021798));
#8049=CARTESIAN_POINT('Origin',(-1.35,2.45,-2.33826859021798));
#8050=CARTESIAN_POINT('',(-2.675,2.20285867594495,-1.57327948354173));
#8051=CARTESIAN_POINT('',(-1.81636895265445,2.4,-2.06901034986126));
#8052=CARTESIAN_POINT('Origin',(-1.35,-2.9,-2.33826859021798));
#8053=CARTESIAN_POINT('',(-0.883631047345552,2.4,-2.60752683057471));
#8054=CARTESIAN_POINT('',(-1.35,2.4,-2.33826859021798));
#8055=CARTESIAN_POINT('Origin',(-1.35,-2.9,-2.33826859021798));
#8056=CARTESIAN_POINT('',(-0.883631047345559,0.0499999999999987,-2.60752683057471));
#8057=CARTESIAN_POINT('Origin',(-1.35,5.35,-2.33826859021798));
#8058=CARTESIAN_POINT('',(-1.81636895265444,0.0499999999999985,-2.06901034986126));
#8059=CARTESIAN_POINT('',(-1.60617376914898,0.05,-2.1903665956405));
#8060=CARTESIAN_POINT('',(-2.675,0.247141324055048,-1.57327948354173));
#8061=CARTESIAN_POINT('Origin',(-1.35,5.35,-2.33826859021798));
#8062=CARTESIAN_POINT('',(-2.675,2.45,-1.57327948354173));
#8063=CARTESIAN_POINT('Origin',(0.,2.45,0.));
#8064=CARTESIAN_POINT('',(-2.65000000000324,2.45,-0.595818764376248));
#8065=CARTESIAN_POINT('',(-1.84099418601376,2.45,-1.99705793783344));
#8066=CARTESIAN_POINT('Origin',(0.,2.45,0.));
#8067=CARTESIAN_POINT('',(-2.65,2.45,0.538516480713456));
#8068=CARTESIAN_POINT('',(-2.65,2.45,0.));
#8069=CARTESIAN_POINT('',(-1.79136895265445,2.45,2.02570907967203));
#8070=CARTESIAN_POINT('Origin',(0.,2.45,0.));
#8071=CARTESIAN_POINT('',(-1.325,2.45,2.29496732002876));
#8072=CARTESIAN_POINT('',(1.79136895265445,2.45,2.02570907967203));
#8073=CARTESIAN_POINT('',(1.325,2.45,2.29496732002876));
#8074=CARTESIAN_POINT('',(2.65,2.45,0.538516480713456));
#8075=CARTESIAN_POINT('Origin',(0.,2.45,0.));
#8076=CARTESIAN_POINT('',(2.65,2.45,-0.538516480713456));
#8077=CARTESIAN_POINT('',(2.65,2.45,0.));
#8078=CARTESIAN_POINT('',(1.79136895265445,2.45,-2.02570907967203));
#8079=CARTESIAN_POINT('Origin',(0.,2.45,0.));
#8080=CARTESIAN_POINT('',(0.858631047345553,2.45,-2.56422556038549));
#8081=CARTESIAN_POINT('',(1.325,2.45,-2.29496732002876));
#8082=CARTESIAN_POINT('',(-0.858631047345553,2.45,-2.56422556038549));
#8083=CARTESIAN_POINT('Origin',(0.,2.45,0.));
#8084=CARTESIAN_POINT('',(-1.325,2.45,-2.29496732002876));
#8085=CARTESIAN_POINT('Origin',(0.,0.,0.));
#8086=CARTESIAN_POINT('',(2.65,0.,-0.538516480713445));
#8087=CARTESIAN_POINT('',(2.65,0.,0.538516480713445));
#8088=CARTESIAN_POINT('',(2.65,0.,0.295803989154973));
#8089=CARTESIAN_POINT('',(1.79136895265444,0.,2.02570907967204));
#8090=CARTESIAN_POINT('Origin',(0.,0.,0.));
#8091=CARTESIAN_POINT('',(1.06882623085102,0.,2.44286931460625));
#8092=CARTESIAN_POINT('',(-1.79136895265444,0.,2.02570907967204));
#8093=CARTESIAN_POINT('',(-1.58117376914898,0.,2.14706532545128));
#8094=CARTESIAN_POINT('',(-2.65,0.,0.538516480713445));
#8095=CARTESIAN_POINT('Origin',(0.,0.,0.));
#8096=CARTESIAN_POINT('',(-2.65,0.,-0.538516480713445));
#8097=CARTESIAN_POINT('',(-2.65,0.,-0.295803989154973));
#8098=CARTESIAN_POINT('',(-1.79136895265444,0.,-2.02570907967204));
#8099=CARTESIAN_POINT('Origin',(0.,0.,0.));
#8100=CARTESIAN_POINT('',(-0.858631047345558,0.,-2.56422556038549));
#8101=CARTESIAN_POINT('',(-1.06882623085102,0.,-2.44286931460625));
#8102=CARTESIAN_POINT('',(0.858631047345562,0.,-2.56422556038549));
#8103=CARTESIAN_POINT('Origin',(0.,0.,0.));
#8104=CARTESIAN_POINT('',(1.79136895265444,0.,-2.02570907967204));
#8105=CARTESIAN_POINT('',(1.58117376914898,0.,-2.14706532545128));
#8106=CARTESIAN_POINT('Origin',(0.,0.,0.));
#8107=CARTESIAN_POINT('Origin',(0.,-2.9,0.));
#8108=CARTESIAN_POINT('',(1.59968345746445E-16,2.24573984128903,3.08567034625716));
#8109=CARTESIAN_POINT('Origin',(-1.33613445378151,-2.9,2.31425275969287));
#8110=CARTESIAN_POINT('Origin',(1.33613445378151,-2.9,2.31425275969287));
#8111=CARTESIAN_POINT('Origin',(0.,-2.9,0.));
#8112=CARTESIAN_POINT('',(1.80642247326499,2.44453781512605,2.04273184504743));
#8113=CARTESIAN_POINT('',(2.67226890756303,2.24573984128903,1.54283517312858));
#8114=CARTESIAN_POINT('Origin',(1.33613445378151,-2.9,2.31425275969287));
#8115=CARTESIAN_POINT('',(2.67226890756303,2.44453781512605,0.543041829290881));
#8116=CARTESIAN_POINT('Origin',(2.67226890756303,-2.9,0.));
#8117=CARTESIAN_POINT('Origin',(0.,2.44453781512605,0.));
#8118=CARTESIAN_POINT('Origin',(0.,-2.9,0.));
#8119=CARTESIAN_POINT('',(0.865846434298035,2.44453781512605,-2.58577367433831));
#8120=CARTESIAN_POINT('',(6.63014680110683E-16,2.24573984128903,-3.08567034625716));
#8121=CARTESIAN_POINT('Origin',(1.33613445378151,-2.9,-2.31425275969287));
#8122=CARTESIAN_POINT('',(-0.865846434298034,2.44453781512605,-2.58577367433831));
#8123=CARTESIAN_POINT('Origin',(-1.33613445378151,-2.9,-2.31425275969287));
#8124=CARTESIAN_POINT('Origin',(0.,2.44453781512605,0.));
#8125=CARTESIAN_POINT('Origin',(0.,-2.9,0.));
#8126=CARTESIAN_POINT('',(-2.67226890756303,2.24573984128903,-1.54283517312858));
#8127=CARTESIAN_POINT('',(-2.67226890756303,2.4447671280735,-0.540780207049814));
#8128=CARTESIAN_POINT('Origin',(-2.67226890756303,-2.9,0.));
#8129=CARTESIAN_POINT('Ctrl Pts',(-2.67226890756303,2.4447671280735,-0.540780207049819));
#8130=CARTESIAN_POINT('Ctrl Pts',(-2.67188165522803,2.44495976241979,-0.540789927546888));
#8131=CARTESIAN_POINT('Ctrl Pts',(-2.67148794036228,2.44514904528708,-0.54086418367862));
#8132=CARTESIAN_POINT('Ctrl Pts',(-2.67038852238207,2.44566128822559,-0.541231202677014));
#8133=CARTESIAN_POINT('Ctrl Pts',(-2.66970822201384,2.44595619716623,-0.541674224166172));
#8134=CARTESIAN_POINT('Ctrl Pts',(-2.66561324339082,2.44765239284951,-0.545108397107626));
#8135=CARTESIAN_POINT('Ctrl Pts',(-2.66401855855887,2.44802977908222,-0.549184489970353));
#8136=CARTESIAN_POINT('Ctrl Pts',(-2.66047421567082,2.44892435679286,-0.557589611972086));
#8137=CARTESIAN_POINT('Ctrl Pts',(-2.65893507904906,2.44921707503779,-0.562108065848044));
#8138=CARTESIAN_POINT('Ctrl Pts',(-2.65458003737285,2.44987629703967,-0.576304280926598));
#8139=CARTESIAN_POINT('Ctrl Pts',(-2.65211510888084,2.45,-0.586411476689759));
#8140=CARTESIAN_POINT('Ctrl Pts',(-2.65,2.45,-0.595818764390658));
#8141=CARTESIAN_POINT('',(-1.80446385095045,2.4447671280735,-2.04386265616796));
#8142=CARTESIAN_POINT('Ctrl Pts',(-1.84099418601376,2.45,-1.99705793783343));
#8143=CARTESIAN_POINT('Ctrl Pts',(-1.8339047903245,2.45,-2.00359331970646));
#8144=CARTESIAN_POINT('Ctrl Pts',(-1.82638416627859,2.44987629703967,-2.01078160828064));
#8145=CARTESIAN_POINT('Ctrl Pts',(-1.81626740422107,2.44921707503779,-2.02165129254605));
#8146=CARTESIAN_POINT('Ctrl Pts',(-1.81312387668954,2.44892435679286,-2.02524345089836));
#8147=CARTESIAN_POINT('Ctrl Pts',(-1.80761699895816,2.44802977908222,-2.03251550288001));
#8148=CARTESIAN_POINT('Ctrl Pts',(-1.80488434140683,2.44765239284951,-2.03593458688687));
#8149=CARTESIAN_POINT('Ctrl Pts',(-1.80395774971005,2.44595619716623,-2.04119802887309));
#8150=CARTESIAN_POINT('Ctrl Pts',(-1.80391423203013,2.44566128822559,-2.04200869701876));
#8151=CARTESIAN_POINT('Ctrl Pts',(-1.80414609324395,2.44514904528708,-2.04314433041819));
#8152=CARTESIAN_POINT('Ctrl Pts',(-1.80427864298037,2.44495976241979,-2.04352242555965));
#8153=CARTESIAN_POINT('Ctrl Pts',(-1.80446385095046,2.4447671280735,-2.04386265616796));
#8154=CARTESIAN_POINT('Origin',(-1.33613445378151,-2.9,-2.31425275969287));
#8155=CARTESIAN_POINT('Origin',(0.,5.35,0.));
#8156=CARTESIAN_POINT('',(2.41574498103394E-16,0.204260158710972,3.08567034625716));
#8157=CARTESIAN_POINT('Origin',(1.33613445378151,5.35,2.31425275969287));
#8158=CARTESIAN_POINT('Origin',(-1.33613445378151,5.35,2.31425275969287));
#8159=CARTESIAN_POINT('Origin',(0.,5.35,0.));
#8160=CARTESIAN_POINT('',(1.80642247326498,0.00546218487394966,2.04273184504743));
#8161=CARTESIAN_POINT('',(2.67226890756303,0.00546218487394974,0.543041829290871));
#8162=CARTESIAN_POINT('Origin',(0.,0.00546218487394983,0.));
#8163=CARTESIAN_POINT('',(2.67226890756303,0.204260158710973,1.54283517312858));
#8164=CARTESIAN_POINT('Origin',(2.67226890756303,5.35,0.));
#8165=CARTESIAN_POINT('Origin',(1.33613445378151,5.35,2.31425275969287));
#8166=CARTESIAN_POINT('Origin',(0.,5.35,0.));
#8167=CARTESIAN_POINT('',(0.865846434298044,0.00546218487394985,-2.58577367433831));
#8168=CARTESIAN_POINT('',(-0.865846434298039,0.00546218487394872,-2.58577367433831));
#8169=CARTESIAN_POINT('Origin',(0.,0.00546218487394896,0.));
#8170=CARTESIAN_POINT('',(8.28890235087106E-16,0.204260158710973,-3.08567034625716));
#8171=CARTESIAN_POINT('Origin',(-1.33613445378151,5.35,-2.31425275969287));
#8172=CARTESIAN_POINT('Origin',(1.33613445378151,5.35,-2.31425275969287));
#8173=CARTESIAN_POINT('Origin',(0.,5.35,0.));
#8174=CARTESIAN_POINT('',(-1.80642247326498,0.00546218487394966,-2.04273184504743));
#8175=CARTESIAN_POINT('',(-2.67226890756303,0.00546218487394972,-0.543041829290871));
#8176=CARTESIAN_POINT('Origin',(0.,0.00546218487394983,0.));
#8177=CARTESIAN_POINT('',(-2.67226890756303,0.204260158710973,-1.54283517312858));
#8178=CARTESIAN_POINT('Origin',(-2.67226890756303,5.35,0.));
#8179=CARTESIAN_POINT('Origin',(-1.33613445378151,5.35,-2.31425275969287));
#8180=CARTESIAN_POINT('Origin',(2.65,2.4,0.538516480713455));
#8181=CARTESIAN_POINT('Origin',(2.65,2.4,0.538516480713457));
#8182=CARTESIAN_POINT('Origin',(2.65,2.4,0.538516480713459));
#8183=CARTESIAN_POINT('Origin',(2.65,2.4,0.538516480713456));
#8184=CARTESIAN_POINT('Origin',(2.65,2.4,0.));
#8185=CARTESIAN_POINT('Origin',(2.65,2.4,-0.538516480713456));
#8186=CARTESIAN_POINT('Origin',(0.,2.4,0.));
#8187=CARTESIAN_POINT('Origin',(1.79136895265445,2.4,2.02570907967203));
#8188=CARTESIAN_POINT('Origin',(1.325,-2.9,2.29496732002876));
#8189=CARTESIAN_POINT('Origin',(2.65,2.20285867594495,1.52997821335251));
#8190=CARTESIAN_POINT('Origin',(1.79136895265445,2.4,2.02570907967203));
#8191=CARTESIAN_POINT('Origin',(2.65,-2.9,0.));
#8192=CARTESIAN_POINT('Origin',(2.65,2.20285867594495,1.52997821335251));
#8193=CARTESIAN_POINT('Origin',(2.65,-2.9,0.));
#8194=CARTESIAN_POINT('Origin',(2.65,2.4,-0.538516480713459));
#8195=CARTESIAN_POINT('Origin',(2.65,2.20285867594495,-1.52997821335251));
#8196=CARTESIAN_POINT('Origin',(2.65,2.4,-0.538516480713455));
#8197=CARTESIAN_POINT('Origin',(2.65,2.4,-0.538516480713457));
#8198=CARTESIAN_POINT('Origin',(1.79136895265445,2.4,2.02570907967203));
#8199=CARTESIAN_POINT('Origin',(1.79136895265445,2.4,2.02570907967203));
#8200=CARTESIAN_POINT('Origin',(2.65,2.20285867594495,1.52997821335251));
#8201=CARTESIAN_POINT('Origin',(2.65,2.20285867594495,1.52997821335251));
#8202=CARTESIAN_POINT('Origin',(2.65,2.20285867594495,-1.52997821335251));
#8203=CARTESIAN_POINT('Origin',(2.65,2.20285867594495,-1.52997821335251));
#8204=CARTESIAN_POINT('Origin',(2.65,2.20285867594495,-1.52997821335251));
#8205=CARTESIAN_POINT('Origin',(1.325,-2.9,-2.29496732002876));
#8206=CARTESIAN_POINT('Origin',(1.79136895265445,2.4,-2.02570907967203));
#8207=CARTESIAN_POINT('Origin',(0.,2.4,0.));
#8208=CARTESIAN_POINT('Origin',(1.79136895265445,2.4,-2.02570907967203));
#8209=CARTESIAN_POINT('Origin',(1.325,2.4,2.29496732002876));
#8210=CARTESIAN_POINT('Origin',(0.858631047345551,2.4,2.56422556038549));
#8211=CARTESIAN_POINT('Origin',(2.65,2.45,1.52997821335251));
#8212=CARTESIAN_POINT('Origin',(2.65,0.247141324055047,1.52997821335251));
#8213=CARTESIAN_POINT('Origin',(2.65,5.35,0.));
#8214=CARTESIAN_POINT('Origin',(2.65,0.05,0.538516480713451));
#8215=CARTESIAN_POINT('Origin',(2.65,0.247141324055048,1.52997821335251));
#8216=CARTESIAN_POINT('Origin',(2.65,0.05,0.));
#8217=CARTESIAN_POINT('Origin',(2.65,0.05,-0.538516480713451));
#8218=CARTESIAN_POINT('Origin',(2.65,0.05,0.538516480713445));
#8219=CARTESIAN_POINT('Origin',(2.65,5.35,0.));
#8220=CARTESIAN_POINT('Origin',(2.65,0.247141324055048,-1.52997821335251));
#8221=CARTESIAN_POINT('Origin',(2.65,0.0500000000000003,-0.538516480713448));
#8222=CARTESIAN_POINT('Origin',(2.65,2.45,-1.52997821335251));
#8223=CARTESIAN_POINT('Origin',(2.65,0.247141324055048,-1.52997821335251));
#8224=CARTESIAN_POINT('Origin',(1.79136895265445,2.4,-2.02570907967203));
#8225=CARTESIAN_POINT('Origin',(1.79136895265445,2.4,-2.02570907967203));
#8226=CARTESIAN_POINT('Origin',(0.858631047345549,2.4,2.56422556038549));
#8227=CARTESIAN_POINT('Origin',(0.85863104734555,2.4,2.56422556038549));
#8228=CARTESIAN_POINT('Origin',(2.65,0.247141324055048,1.52997821335251));
#8229=CARTESIAN_POINT('Origin',(2.65,0.247141324055048,1.52997821335251));
#8230=CARTESIAN_POINT('Origin',(2.65,0.05,0.538516480713445));
#8231=CARTESIAN_POINT('Origin',(2.65,0.0500000000000002,0.538516480713447));
#8232=CARTESIAN_POINT('Origin',(2.65,0.05,-0.538516480713445));
#8233=CARTESIAN_POINT('Origin',(2.65,0.05,-0.538516480713445));
#8234=CARTESIAN_POINT('Origin',(2.65,0.247141324055048,-1.52997821335251));
#8235=CARTESIAN_POINT('Origin',(2.65,0.247141324055049,-1.52997821335251));
#8236=CARTESIAN_POINT('Origin',(1.325,2.4,-2.29496732002876));
#8237=CARTESIAN_POINT('Origin',(0.858631047345553,2.4,-2.56422556038549));
#8238=CARTESIAN_POINT('Origin',(-1.325,-2.9,2.29496732002876));
#8239=CARTESIAN_POINT('Origin',(2.35402744940532E-17,2.20285867594495,3.05995642670501));
#8240=CARTESIAN_POINT('Origin',(-0.858631047345551,2.4,2.56422556038549));
#8241=CARTESIAN_POINT('Origin',(1.325,-2.9,2.29496732002876));
#8242=CARTESIAN_POINT('Origin',(1.66018457661843E-16,2.20285867594495,3.05995642670502));
#8243=CARTESIAN_POINT('Origin',(1.325,5.35,2.29496732002876));
#8244=CARTESIAN_POINT('Origin',(1.79136895265444,0.0499999999999991,2.02570907967204));
#8245=CARTESIAN_POINT('Origin',(0.,0.0499999999999997,0.));
#8246=CARTESIAN_POINT('Origin',(1.79136895265444,0.05,2.02570907967204));
#8247=CARTESIAN_POINT('Origin',(0.,0.0499999999999997,0.));
#8248=CARTESIAN_POINT('Origin',(1.79136895265444,0.0499999999999996,-2.02570907967204));
#8249=CARTESIAN_POINT('Origin',(1.325,5.35,-2.29496732002876));
#8250=CARTESIAN_POINT('Origin',(1.79136895265444,0.05,-2.02570907967204));
#8251=CARTESIAN_POINT('Origin',(1.325,-2.9,-2.29496732002876));
#8252=CARTESIAN_POINT('Origin',(0.858631047345552,2.4,-2.56422556038549));
#8253=CARTESIAN_POINT('Origin',(6.57489557776427E-16,2.20285867594495,-3.05995642670502));
#8254=CARTESIAN_POINT('Origin',(0.858631047345552,2.4,-2.56422556038549));
#8255=CARTESIAN_POINT('Origin',(0.858631047345552,2.4,-2.56422556038549));
#8256=CARTESIAN_POINT('Origin',(-0.858631047345553,2.4,2.56422556038549));
#8257=CARTESIAN_POINT('Origin',(-0.858631047345553,2.4,2.56422556038549));
#8258=CARTESIAN_POINT('Origin',(5.97981122629482E-17,2.20285867594495,3.05995642670502));
#8259=CARTESIAN_POINT('Origin',(-1.01643953670516E-17,2.20285867594495,
3.05995642670502));
#8260=CARTESIAN_POINT('Origin',(1.79136895265444,0.0499999999999997,2.02570907967204));
#8261=CARTESIAN_POINT('Origin',(1.79136895265444,0.05,2.02570907967204));
#8262=CARTESIAN_POINT('Origin',(1.79136895265444,0.0499999999999999,-2.02570907967204));
#8263=CARTESIAN_POINT('Origin',(1.79136895265444,0.05,-2.02570907967204));
#8264=CARTESIAN_POINT('Origin',(3.69370361905238E-16,2.20285867594495,-3.05995642670502));
#8265=CARTESIAN_POINT('Origin',(-1.01643953670516E-17,2.20285867594495,
-3.05995642670502));
#8266=CARTESIAN_POINT('Origin',(-1.325,-2.9,-2.29496732002876));
#8267=CARTESIAN_POINT('Origin',(-0.85863104734555,2.4,-2.56422556038549));
#8268=CARTESIAN_POINT('Origin',(0.,2.4,0.));
#8269=CARTESIAN_POINT('Origin',(-0.858631047345553,2.4,-2.56422556038549));
#8270=CARTESIAN_POINT('Origin',(0.,2.4,0.));
#8271=CARTESIAN_POINT('Origin',(-1.79136895265445,2.4,2.02570907967203));
#8272=CARTESIAN_POINT('Origin',(-2.65,2.4,0.538516480713457));
#8273=CARTESIAN_POINT('Origin',(-1.325,2.4,2.29496732002876));
#8274=CARTESIAN_POINT('Origin',(-1.79136895265445,2.4,2.02570907967203));
#8275=CARTESIAN_POINT('Origin',(2.16840434497101E-16,2.45,3.05995642670502));
#8276=CARTESIAN_POINT('Origin',(1.55854062294791E-16,0.247141324055048,
3.05995642670502));
#8277=CARTESIAN_POINT('Origin',(1.325,5.35,2.29496732002876));
#8278=CARTESIAN_POINT('Origin',(0.858631047345559,0.05,2.56422556038549));
#8279=CARTESIAN_POINT('Origin',(2.39561377285866E-16,0.247141324055048,
3.05995642670501));
#8280=CARTESIAN_POINT('Origin',(1.325,0.05,2.29496732002876));
#8281=CARTESIAN_POINT('Origin',(0.858631047345558,0.05,2.56422556038549));
#8282=CARTESIAN_POINT('Origin',(1.325,0.05,-2.29496732002876));
#8283=CARTESIAN_POINT('Origin',(0.858631047345559,0.05,-2.56422556038549));
#8284=CARTESIAN_POINT('Origin',(1.325,5.35,-2.29496732002876));
#8285=CARTESIAN_POINT('Origin',(4.60785923306339E-16,0.247141324055048,
-3.05995642670502));
#8286=CARTESIAN_POINT('Origin',(0.858631047345561,0.0500000000000003,-2.56422556038549));
#8287=CARTESIAN_POINT('Origin',(-0.858631047345549,2.4,-2.56422556038549));
#8288=CARTESIAN_POINT('Origin',(-0.858631047345551,2.4,-2.56422556038549));
#8289=CARTESIAN_POINT('Origin',(-2.65,2.4,0.538516480713455));
#8290=CARTESIAN_POINT('Origin',(-2.65,2.4,0.538516480713459));
#8291=CARTESIAN_POINT('Origin',(-2.65,2.4,0.538516480713456));
#8292=CARTESIAN_POINT('Origin',(-1.79136895265445,2.4,2.02570907967203));
#8293=CARTESIAN_POINT('Origin',(-1.79136895265445,2.4,2.02570907967203));
#8294=CARTESIAN_POINT('Origin',(-8.84234197592324E-17,0.247141324055048,
3.05995642670502));
#8295=CARTESIAN_POINT('Origin',(-1.01643953670516E-17,0.247141324055048,
3.05995642670502));
#8296=CARTESIAN_POINT('Origin',(0.858631047345558,0.05,2.56422556038549));
#8297=CARTESIAN_POINT('Origin',(0.858631047345562,0.05,-2.56422556038549));
#8298=CARTESIAN_POINT('Origin',(0.858631047345562,0.05,-2.56422556038549));
#8299=CARTESIAN_POINT('Origin',(4.33176733571846E-16,0.247141324055048,
-3.05995642670502));
#8300=CARTESIAN_POINT('Origin',(5.23648021030599E-16,0.247141324055048,
-3.05995642670501));
#8301=CARTESIAN_POINT('Origin',(-1.325,2.4,-2.29496732002876));
#8302=CARTESIAN_POINT('Origin',(-1.79132934405401,2.40001396671009,-2.02565080655304));
#8303=CARTESIAN_POINT('Origin',(-2.65,2.4,0.));
#8304=CARTESIAN_POINT('Origin',(-2.64992972818517,2.40001396579085,-0.538511314860504));
#8305=CARTESIAN_POINT('Origin',(-2.65,-2.9,0.));
#8306=CARTESIAN_POINT('Origin',(-2.65,2.20285867594495,1.52997821335251));
#8307=CARTESIAN_POINT('Origin',(-1.325,-2.9,2.29496732002876));
#8308=CARTESIAN_POINT('Origin',(-2.65,2.20285867594495,1.52997821335251));
#8309=CARTESIAN_POINT('Origin',(-1.325,5.35,2.29496732002876));
#8310=CARTESIAN_POINT('Origin',(-0.858631047345555,0.0499999999999995,2.56422556038549));
#8311=CARTESIAN_POINT('Origin',(0.,0.0499999999999997,0.));
#8312=CARTESIAN_POINT('Origin',(-0.858631047345555,0.0499999999999992,-2.56422556038549));
#8313=CARTESIAN_POINT('Origin',(-1.325,5.35,-2.29496732002876));
#8314=CARTESIAN_POINT('Origin',(-0.858631047345559,0.05,-2.56422556038549));
#8315=CARTESIAN_POINT('Origin',(-1.325,-2.9,-2.29496732002876));
#8316=CARTESIAN_POINT('Origin',(-2.65,2.20285867594495,-1.52997821335251));
#8317=CARTESIAN_POINT('Origin',(-2.65,-2.9,0.));
#8318=CARTESIAN_POINT('Origin',(-2.65,2.20285867594495,-1.52997821335251));
#8319=CARTESIAN_POINT('Origin',(-2.65,2.20285867594495,1.52997821335251));
#8320=CARTESIAN_POINT('Origin',(-2.65,2.20285867594495,1.52997821335251));
#8321=CARTESIAN_POINT('Origin',(-0.858631047345559,0.05,2.56422556038549));
#8322=CARTESIAN_POINT('Origin',(-0.858631047345559,0.05,2.56422556038549));
#8323=CARTESIAN_POINT('Origin',(-0.858631047345557,0.0499999999999997,-2.56422556038549));
#8324=CARTESIAN_POINT('Origin',(-0.858631047345558,0.05,-2.56422556038549));
#8325=CARTESIAN_POINT('Origin',(-2.65,2.20285867594495,-1.52997821335251));
#8326=CARTESIAN_POINT('Origin',(-2.65,2.20285867594495,-1.52997821335251));
#8327=CARTESIAN_POINT('Origin',(-2.65,2.45,1.52997821335251));
#8328=CARTESIAN_POINT('Origin',(-2.65,0.247141324055048,1.52997821335251));
#8329=CARTESIAN_POINT('Origin',(-1.325,5.35,2.29496732002876));
#8330=CARTESIAN_POINT('Origin',(-1.79136895265444,0.05,2.02570907967204));
#8331=CARTESIAN_POINT('Origin',(-2.65,0.247141324055048,1.52997821335251));
#8332=CARTESIAN_POINT('Origin',(-1.325,0.05,2.29496732002876));
#8333=CARTESIAN_POINT('Origin',(-1.79136895265444,0.05,2.02570907967204));
#8334=CARTESIAN_POINT('Origin',(-1.325,0.05,-2.29496732002876));
#8335=CARTESIAN_POINT('Origin',(-1.79136895265444,0.05,-2.02570907967204));
#8336=CARTESIAN_POINT('Origin',(-1.325,5.35,-2.29496732002876));
#8337=CARTESIAN_POINT('Origin',(-2.65,0.247141324055048,-1.52997821335251));
#8338=CARTESIAN_POINT('Origin',(-1.79136895265444,0.0499999999999991,-2.02570907967204));
#8339=CARTESIAN_POINT('Origin',(-2.65,2.45,-1.52997821335251));
#8340=CARTESIAN_POINT('Origin',(-2.65,0.247141324055048,-1.52997821335251));
#8341=CARTESIAN_POINT('Origin',(-2.65,0.247141324055048,1.52997821335251));
#8342=CARTESIAN_POINT('Origin',(-2.65,0.247141324055048,1.52997821335251));
#8343=CARTESIAN_POINT('Origin',(-1.79136895265444,0.05,2.02570907967204));
#8344=CARTESIAN_POINT('Origin',(-1.79136895265444,0.0500000000000002,2.02570907967204));
#8345=CARTESIAN_POINT('Origin',(-1.79136895265444,0.0499999999999997,-2.02570907967204));
#8346=CARTESIAN_POINT('Origin',(-1.79136895265444,0.05,-2.02570907967204));
#8347=CARTESIAN_POINT('Origin',(-2.65,0.247141324055048,-1.52997821335251));
#8348=CARTESIAN_POINT('Origin',(-2.65,0.247141324055048,-1.52997821335251));
#8349=CARTESIAN_POINT('Origin',(-2.65,5.35,0.));
#8350=CARTESIAN_POINT('Origin',(-2.65,0.0500000000000003,0.538516480713448));
#8351=CARTESIAN_POINT('Origin',(0.,0.0499999999999997,0.));
#8352=CARTESIAN_POINT('Origin',(-2.65,0.05,0.538516480713445));
#8353=CARTESIAN_POINT('Origin',(0.,0.0499999999999997,0.));
#8354=CARTESIAN_POINT('Origin',(-2.65,0.0500000000000001,-0.538516480713447));
#8355=CARTESIAN_POINT('Origin',(-2.65,5.35,0.));
#8356=CARTESIAN_POINT('Origin',(-2.65,0.05,-0.538516480713451));
#8357=CARTESIAN_POINT('Origin',(-2.65,0.05,0.538516480713445));
#8358=CARTESIAN_POINT('Origin',(-2.65,0.05,0.538516480713451));
#8359=CARTESIAN_POINT('Origin',(-2.65,0.05,-0.538516480713445));
#8360=CARTESIAN_POINT('Origin',(-2.65,0.05,-0.538516480713445));
#8361=CARTESIAN_POINT('Origin',(-2.65,0.05,0.));
#8362=CARTESIAN_POINT('Origin',(0.,4.85,0.));
#10537=UNCERTAINTY_MEASURE_WITH_UNIT(LENGTH_MEASURE(0.01),#10552,
'DISTANCE_ACCURACY_VALUE',
'Maximum model space distance between geometric entities at asserted c
onnectivities');
#10540=UNCERTAINTY_MEASURE_WITH_UNIT(LENGTH_MEASURE(0.01),#10552,
'DISTANCE_ACCURACY_VALUE',
'Maximum model space distance between geometric entities at asserted c
onnectivities');
#10548=(
GEOMETRIC_REPRESENTATION_CONTEXT(3)
GLOBAL_UNCERTAINTY_ASSIGNED_CONTEXT((#10537))
GLOBAL_UNIT_ASSIGNED_CONTEXT((#10552,#10554,#10555))
REPRESENTATION_CONTEXT('','3D')
);
#10551=(
GEOMETRIC_REPRESENTATION_CONTEXT(3)
GLOBAL_UNCERTAINTY_ASSIGNED_CONTEXT((#10540))
GLOBAL_UNIT_ASSIGNED_CONTEXT((#10552,#10554,#10555))
REPRESENTATION_CONTEXT('','3D')
);
#10552=(
LENGTH_UNIT()
NAMED_UNIT(*)
SI_UNIT(.MILLI.,.METRE.)
);
#10554=(
NAMED_UNIT(*)
PLANE_ANGLE_UNIT()
SI_UNIT($,.RADIAN.)
);
#10555=(
NAMED_UNIT(*)
SI_UNIT($,.STERADIAN.)
SOLID_ANGLE_UNIT()
);
#10563=SHAPE_DEFINITION_REPRESENTATION(#10573,#10592);
#10573=PRODUCT_DEFINITION_SHAPE('',$,#10603);
#10592=SHAPE_REPRESENTATION('',(#3718),#10548);
#10595=PRODUCT_DEFINITION_CONTEXT('part definition',#10627,'design');
#10603=PRODUCT_DEFINITION('Nut','Nut',#10613,#10595);
#10613=PRODUCT_DEFINITION_FORMATION('',$,#10636);
#10627=APPLICATION_CONTEXT(
'Core Data for Automotive Mechanical Design Process');
#10628=PRODUCT_CONTEXT('part definition',#10627,'mechanical');
#10636=PRODUCT('Nut','Nut',$,(#10628));
#10644=PRESENTATION_STYLE_ASSIGNMENT((#10651));
#10651=SURFACE_STYLE_USAGE(.BOTH.,#10658);
#10658=SURFACE_SIDE_STYLE('',(#10665));
#10665=SURFACE_STYLE_FILL_AREA(#10672);
#10672=FILL_AREA_STYLE('Opaque(31,36,43)',(#10679));
#10679=FILL_AREA_STYLE_COLOUR('Opaque(31,36,43)',#10686);
#10686=COLOUR_RGB('Opaque(31,36,43)',0.12156862745098,0.141176470588235,
0.168627450980392);
ENDSEC;
END-ISO-10303-21;
